ISO-10303-21;
HEADER;
FILE_DESCRIPTION (('STEP AP214'),
    '1' );
FILE_NAME ('Part 131_Varsay\X2\0131\X0\lan.step',
    '2026-10-08T11:03:28',
    ( '' ),
    ( '' ),
    'SwSTEP 2.0',
    'SolidWorks 2024',
    '' );
FILE_SCHEMA (( 'AUTOMOTIVE_DESIGN' ));
ENDSEC;

DATA;
#1=ORIENTED_EDGE ( 'NONE', *, *, #3804, .F. ) ;
#2=CARTESIAN_POINT ( 'NONE',  ( -13.11668479459951087, 5.670681919514632519, 36.22991310522757402 ) ) ;
#4=VERTEX_POINT ( 'NONE', #1586 ) ;
#5=DIRECTION ( 'NONE',  ( -0.000000000000000000, -0.000000000000000000, -1.000000000000000000 ) ) ;
#10=CARTESIAN_POINT ( 'NONE',  ( 8.370007234561949616, 7.901597986548672736, 17.90262445358908039 ) ) ;
#11=CARTESIAN_POINT ( 'NONE',  ( 12.37117936981251631, 7.901597986548669184, 17.15262445358908039 ) ) ;
#20=EDGE_CURVE ( 'NONE', #2372, #3471, #3030, .T. ) ;
#24=DIRECTION ( 'NONE',  ( 0.000000000000000000, 1.000000000000000000, 0.000000000000000000 ) ) ;
#25=ORIENTED_EDGE ( 'NONE', *, *, #871, .F. ) ;
#27=CARTESIAN_POINT ( 'NONE',  ( -12.39927918895608094, 7.103532125216092119, 32.82105853334656587 ) ) ;
#29=EDGE_LOOP ( 'NONE', ( #1981, #2414, #2943, #1041 ) ) ;
#31=DIRECTION ( 'NONE',  ( -1.076498916035107621E-16, -1.000000000000000000, -8.841607930564763213E-17 ) ) ;
#34=CARTESIAN_POINT ( 'NONE',  ( -0.2830874312243520929, -3.565902013451327512, -9.735057145307090209 ) ) ;
#47=PLANE ( 'NONE',  #853 ) ;
#57=EDGE_CURVE ( 'NONE', #1869, #1513, #3978, .T. ) ;
#58=CARTESIAN_POINT ( 'NONE',  ( 12.76962931635276455, 6.415859468635933816, 35.06035830646958829 ) ) ;
#61=CARTESIAN_POINT ( 'NONE',  ( 6.870007234561953169, -6.393402013451325416, 17.15262445358908039 ) ) ;
#63=CARTESIAN_POINT ( 'NONE',  ( -8.369992765438043492, 6.401597986548673624, 17.90262445358908039 ) ) ;
#69=AXIS2_PLACEMENT_3D ( 'NONE', #833, #180, #3017 ) ;
#74=CARTESIAN_POINT ( 'NONE',  ( -12.37116490068861019, 7.151597986548670072, 17.90262445358908039 ) ) ;
#78=DIRECTION ( 'NONE',  ( 0.000000000000000000, 0.000000000000000000, -1.000000000000000000 ) ) ;
#88=DIRECTION ( 'NONE',  ( -0.000000000000000000, -0.000000000000000000, -1.000000000000000000 ) ) ;
#91=ORIENTED_EDGE ( 'NONE', *, *, #2174, .T. ) ;
#94=ORIENTED_EDGE ( 'NONE', *, *, #395, .F. ) ;
#95=DIRECTION ( 'NONE',  ( 1.076498916035107621E-16, 1.000000000000000000, -0.000000000000000000 ) ) ;
#97=CARTESIAN_POINT ( 'NONE',  ( 14.99250723456195544, 7.901597986548669184, 17.90262445358908039 ) ) ;
#98=VERTEX_POINT ( 'NONE', #430 ) ;
#99=ORIENTED_EDGE ( 'NONE', *, *, #1933, .F. ) ;
#100=DIRECTION ( 'NONE',  ( 0.000000000000000000, 1.000000000000000000, -0.000000000000000000 ) ) ;
#101=AXIS2_PLACEMENT_3D ( 'NONE', #3470, #3879, #4145 ) ;
#102=CARTESIAN_POINT ( 'NONE',  ( -12.18302349840153731, -7.460057201642745106, 17.28264009582346006 ) ) ;
#105=EDGE_CURVE ( 'NONE', #338, #3364, #3317, .T. ) ;
#106=CARTESIAN_POINT ( 'NONE',  ( -7.619992765438047044, -7.143402013451323640, 17.90262445358908039 ) ) ;
#111=CARTESIAN_POINT ( 'NONE',  ( 8.370007234561953169, 7.151597986548671848, 17.90262445358908039 ) ) ;
#114=EDGE_CURVE ( 'NONE', #4543, #2437, #498, .T. ) ;
#116=VERTEX_POINT ( 'NONE', #479 ) ;
#117=CARTESIAN_POINT ( 'NONE',  ( 13.94777217564051952, -3.095918481782248044, 30.07429697042405081 ) ) ;
#121=CARTESIAN_POINT ( 'NONE',  ( 13.83333536583607959, 3.577847986548670978, 31.86762445358909446 ) ) ;
#128=CIRCLE ( 'NONE', #4565, 6.397499999999999964 ) ;
#129=DIRECTION ( 'NONE',  ( 0.000000000000000000, 0.000000000000000000, 1.000000000000000000 ) ) ;
#131=CARTESIAN_POINT ( 'NONE',  ( -13.83927268380397635, 3.555046762887689837, 32.33443371951124590 ) ) ;
#132=CARTESIAN_POINT ( 'NONE',  ( 7.234561953626996335E-06, 0.004097986548672528061, -1.469875546410923661 ) ) ;
#135=FACE_OUTER_BOUND ( 'NONE', #1112, .T. ) ;
#138=ORIENTED_EDGE ( 'NONE', *, *, #1516, .F. ) ;
#140=ORIENTED_EDGE ( 'NONE', *, *, #3397, .F. ) ;
#142=DIRECTION ( 'NONE',  ( 1.000000000000000000, -1.076498916035107744E-16, 0.000000000000000000 ) ) ;
#143=CARTESIAN_POINT ( 'NONE',  ( 13.83333536583607959, 3.577847986548671422, 32.33516565723597580 ) ) ;
#146=ORIENTED_EDGE ( 'NONE', *, *, #3284, .F. ) ;
#148=CARTESIAN_POINT ( 'NONE',  ( -12.02318935820893664, -7.715086390250210258, 17.16832378532598113 ) ) ;
#149=CIRCLE ( 'NONE', #1518, 0.7500000000000006661 ) ;
#151=CARTESIAN_POINT ( 'NONE',  ( 12.37117936981251987, 7.151597986548668295, 17.90262445358908039 ) ) ;
#155=DIRECTION ( 'NONE',  ( -1.000000000000000000, 1.076498916035107744E-16, 0.000000000000000000 ) ) ;
#157=ORIENTED_EDGE ( 'NONE', *, *, #1855, .F. ) ;
#159=EDGE_CURVE ( 'NONE', #3907, #1168, #3927, .T. ) ;
#163=EDGE_CURVE ( 'NONE', #696, #4208, #4390, .T. ) ;
#164=VECTOR ( 'NONE', #2575, 1000.000000000000000 ) ;
#165=CARTESIAN_POINT ( 'NONE',  ( 13.94792900051583651, 3.103387315081731934, 30.07316051872297535 ) ) ;
#167=ORIENTED_EDGE ( 'NONE', *, *, #3789, .T. ) ;
#175=CARTESIAN_POINT ( 'NONE',  ( 8.370007234561949616, -7.893402013451324528, 17.90262445358908039 ) ) ;
#176=EDGE_LOOP ( 'NONE', ( #2140, #3817, #1217, #3827 ) ) ;
#180=DIRECTION ( 'NONE',  ( 0.000000000000000000, 0.000000000000000000, -1.000000000000000000 ) ) ;
#181=CARTESIAN_POINT ( 'NONE',  ( -14.09151123534772765, 2.368322898672384991, 34.55761253202872041 ) ) ;
#182=CARTESIAN_POINT ( 'NONE',  ( 8.370007234561954945, -7.143402013451326305, 31.86762445358908735 ) ) ;
#183=EDGE_CURVE ( 'NONE', #3678, #2227, #613, .T. ) ;
#200=ORIENTED_EDGE ( 'NONE', *, *, #995, .F. ) ;
#201=CARTESIAN_POINT ( 'NONE',  ( -7.619992765438047044, -6.393402013451325416, 31.86762445358908735 ) ) ;
#203=CYLINDRICAL_SURFACE ( 'NONE', #1154, 7.147499999999999076 ) ;
#205=DIRECTION ( 'NONE',  ( 0.000000000000000000, 0.000000000000000000, -1.000000000000000000 ) ) ;
#207=AXIS2_PLACEMENT_3D ( 'NONE', #2433, #3594, #1816 ) ;
#208=CARTESIAN_POINT ( 'NONE',  ( -14.12120247390863881, -2.178204474482083874, 29.02795621720992614 ) ) ;
#211=EDGE_LOOP ( 'NONE', ( #1277, #2429, #378, #3663, #2254 ) ) ;
#216=AXIS2_PLACEMENT_3D ( 'NONE', #2791, #3106, #2092 ) ;
#217=DIRECTION ( 'NONE',  ( 1.000000000000000000, 0.000000000000000000, 0.000000000000000000 ) ) ;
#219=ORIENTED_EDGE ( 'NONE', *, *, #1152, .T. ) ;
#220=CARTESIAN_POINT ( 'NONE',  ( 18.74250723456195189, 0.004097986548670510577, 31.86762445358909446 ) ) ;
#222=ORIENTED_EDGE ( 'NONE', *, *, #2560, .T. ) ;
#225=LINE ( 'NONE', #1603, #3538 ) ;
#227=CARTESIAN_POINT ( 'NONE',  ( -13.83332089671217169, -3.569652013451326322, 31.86762445358909446 ) ) ;
#231=CARTESIAN_POINT ( 'NONE',  ( 13.83333536583607959, 3.577847986548670978, 31.86762445358909446 ) ) ;
#235=ORIENTED_EDGE ( 'NONE', *, *, #3251, .F. ) ;
#236=CIRCLE ( 'NONE', #4105, 7.147499999999999076 ) ;
#243=AXIS2_PLACEMENT_3D ( 'NONE', #3248, #4018, #4329 ) ;
#251=EDGE_CURVE ( 'NONE', #4208, #3225, #2015, .T. ) ;
#252=CARTESIAN_POINT ( 'NONE',  ( -3.152215195724335395, -3.565902013451327068, -10.04237554641092345 ) ) ;
#254=VERTEX_POINT ( 'NONE', #4484 ) ;
#255=CARTESIAN_POINT ( 'NONE',  ( -6.869992765438047932, -6.393402013451324528, 17.90262445358908039 ) ) ;
#260=EDGE_CURVE ( 'NONE', #1840, #560, #2604, .T. ) ;
#261=FACE_OUTER_BOUND ( 'NONE', #3718, .T. ) ;
#263=EDGE_CURVE ( 'NONE', #1498, #728, #3212, .T. ) ;
#264=EDGE_LOOP ( 'NONE', ( #3177, #543, #4448, #1020 ) ) ;
#277=ORIENTED_EDGE ( 'NONE', *, *, #2701, .T. ) ;
#278=CARTESIAN_POINT ( 'NONE',  ( 13.23919276269517020, -5.370076350862035497, 36.58546145169297859 ) ) ;
#279=DIRECTION ( 'NONE',  ( -1.000000000000000000, 0.000000000000000000, 0.000000000000000000 ) ) ;
#281=ORIENTED_EDGE ( 'NONE', *, *, #2560, .F. ) ;
#286=EDGE_CURVE ( 'NONE', #1844, #313, #1692, .T. ) ;
#289=DIRECTION ( 'NONE',  ( 1.000000000000000000, -0.000000000000000000, -0.000000000000000000 ) ) ;
#291=CARTESIAN_POINT ( 'NONE',  ( -12.13298098450732354, 7.549547314929181852, 17.23390984512910507 ) ) ;
#292=VECTOR ( 'NONE', #482, 1000.000000000000000 ) ;
#297=DIRECTION ( 'NONE',  ( 1.000000000000000000, -1.076498916035107621E-16, -0.000000000000000000 ) ) ;
#300=CARTESIAN_POINT ( 'NONE',  ( 12.37117936981252164, -7.143402013451325416, 17.90262445358908039 ) ) ;
#306=CARTESIAN_POINT ( 'NONE',  ( 6.870007234561950504, -6.393402013451325416, 17.90262445358908039 ) ) ;
#308=ORIENTED_EDGE ( 'NONE', *, *, #2151, .T. ) ;
#313=VERTEX_POINT ( 'NONE', #2097 ) ;
#316=CARTESIAN_POINT ( 'NONE',  ( -14.03269519519255759, 2.695605797375577151, 29.50494583009495742 ) ) ;
#327=CARTESIAN_POINT ( 'NONE',  ( -8.369992765438045268, -7.893402013451320975, 17.15262445358908039 ) ) ;
#328=ADVANCED_FACE ( 'NONE', ( #3115 ), #973, .F. ) ;
#334=EDGE_LOOP ( 'NONE', ( #4411, #4153, #2795, #3553 ) ) ;
#338=VERTEX_POINT ( 'NONE', #2390 ) ;
#340=CARTESIAN_POINT ( 'NONE',  ( 13.48444558334203691, 4.730385405907853169, 37.23438744284854351 ) ) ;
#345=CARTESIAN_POINT ( 'NONE',  ( 8.370007234561949616, 6.401597986548672736, 17.15262445358908039 ) ) ;
#346=CARTESIAN_POINT ( 'NONE',  ( 8.370007234561949616, -6.393402013451325416, 17.15262445358908039 ) ) ;
#347=DIRECTION ( 'NONE',  ( 1.000000000000000000, 0.000000000000000000, 0.000000000000000000 ) ) ;
#350=ORIENTED_EDGE ( 'NONE', *, *, #1980, .F. ) ;
#358=AXIS2_PLACEMENT_3D ( 'NONE', #3782, #2976, #2651 ) ;
#363=MANIFOLD_SOLID_BREP ( 'Ölçek1', #3046 ) ;
#365=EDGE_CURVE ( 'NONE', #4505, #675, #3257, .T. ) ;
#366=CARTESIAN_POINT ( 'NONE',  ( 8.370007234561949616, 6.401597986548672736, 3.292624453589077405 ) ) ;
#367=CARTESIAN_POINT ( 'NONE',  ( 14.99250723456195544, 7.151597986548670072, 3.292624453589077405 ) ) ;
#368=FACE_OUTER_BOUND ( 'NONE', #29, .T. ) ;
#369=CARTESIAN_POINT ( 'NONE',  ( -8.369992765438045268, -6.393402013451324528, 17.15262445358908039 ) ) ;
#370=CARTESIAN_POINT ( 'NONE',  ( -14.12109987650483056, -2.178937149005899521, 34.70680459945198493 ) ) ;
#371=DIRECTION ( 'NONE',  ( -1.000000000000000000, 1.076498916035107621E-16, 0.000000000000000000 ) ) ;
#372=AXIS2_PLACEMENT_3D ( 'NONE', #860, #2622, #4439 ) ;
#378=ORIENTED_EDGE ( 'NONE', *, *, #2676, .T. ) ;
#380=CARTESIAN_POINT ( 'NONE',  ( -14.28749276543804392, 0.4849387513329158628, 39.01512445358908820 ) ) ;
#385=CARTESIAN_POINT ( 'NONE',  ( -6.869992765438046156, 0.004097986548673267920, 17.15262445358908039 ) ) ;
#389=FACE_OUTER_BOUND ( 'NONE', #4126, .T. ) ;
#392=CARTESIAN_POINT ( 'NONE',  ( -14.03259092081030701, -2.687846779405278053, 34.22958848126887688 ) ) ;
#395=EDGE_CURVE ( 'NONE', #1844, #3471, #2461, .T. ) ;
#398=CARTESIAN_POINT ( 'NONE',  ( -14.26328196213224508, -0.9495361258265833104, 38.96707689327597279 ) ) ;
#399=B_SPLINE_CURVE_WITH_KNOTS ( 'NONE', 3,
 ( #440, #4305, #2931, #3316, #4379, #1188, #791, #2184, #3622, #1866, #3997, #1165, #3948, #1560, #3341, #2580, #2252, #1140, #2953, #3598, #2556, #398, #4399, #768 ),
 .UNSPECIFIED., .F., .F.,
 ( 4, 2, 2, 2, 2, 2, 2, 2, 2, 2, 2, 4 ),
 ( -0.01136693575711654296, -0.009946068787476983544, -0.008525201817837424131, -0.007104334848197864719, -0.006393901363378076338, -0.005683467878558287091, -0.004973034393738498711, -0.004262600908918711198, -0.002841733939279146581, -0.002131300454459359936, -0.001420866969639575025, -1.734723475976807094E-18 ),
 .UNSPECIFIED. ) ;
#404=EDGE_CURVE ( 'NONE', #1899, #4499, #3693, .T. ) ;
#405=EDGE_LOOP ( 'NONE', ( #1015, #2600, #235, #1549 ) ) ;
#406=EDGE_CURVE ( 'NONE', #2052, #4636, #1215, .T. ) ;
#407=CARTESIAN_POINT ( 'NONE',  ( 7.234561953626996335E-06, 0.004097986548672528061, 17.15262445358908039 ) ) ;
#414=CARTESIAN_POINT ( 'NONE',  ( 14.25924652348691524, -0.9230119033506298809, 35.32694493162775018 ) ) ;
#416=PRODUCT_DEFINITION_FORMATION_WITH_SPECIFIED_SOURCE ( 'ANY', '', #1031, .NOT_KNOWN. ) ;
#426=ORIENTED_EDGE ( 'NONE', *, *, #1490, .F. ) ;
#430=CARTESIAN_POINT ( 'NONE',  ( 11.90639837545767321, 7.901597986548669184, 17.15262445358908039 ) ) ;
#431=CIRCLE ( 'NONE', #3662, 0.7500000000000006661 ) ;
#433=DIRECTION ( 'NONE',  ( 9.517981353260378315E-33, 8.841607930564763213E-17, -1.000000000000000000 ) ) ;
#435=CARTESIAN_POINT ( 'NONE',  ( -14.28749276543804747, -0.2329318086950452060, 35.44137445358909133 ) ) ;
#438=ORIENTED_EDGE ( 'NONE', *, *, #1098, .F. ) ;
#440=CARTESIAN_POINT ( 'NONE',  ( -12.37116490068861197, -7.143402013451323640, 31.86762445358908735 ) ) ;
#441=AXIS2_PLACEMENT_3D ( 'NONE', #2692, #532, #1950 ) ;
#442=DIRECTION ( 'NONE',  ( -1.000000000000000000, 1.076498916035107621E-16, 0.000000000000000000 ) ) ;
#446=DIRECTION ( 'NONE',  ( 0.000000000000000000, 1.000000000000000000, 0.000000000000000000 ) ) ;
#447=LINE ( 'NONE', #3345, #4260 ) ;
#451=AXIS2_PLACEMENT_3D ( 'NONE', #1765, #2065, #670 ) ;
#453=CARTESIAN_POINT ( 'NONE',  ( -12.35763029845398364, -7.166954453838238592, 17.68847735315405245 ) ) ;
#454=ORIENTED_EDGE ( 'NONE', *, *, #3428, .F. ) ;
#459=CARTESIAN_POINT ( 'NONE',  ( -12.37116490068860841, 7.151597986548674513, 17.79434398117761518 ) ) ;
#460=VECTOR ( 'NONE', #2087, 1000.000000000000000 ) ;
#461=CARTESIAN_POINT ( 'NONE',  ( 14.99250723456195189, 0.004097986548670913901, 31.86762445358908735 ) ) ;
#462=CARTESIAN_POINT ( 'NONE',  ( -7.619992765438038163, 7.901597986548672736, 17.15262445358908039 ) ) ;
#465=ORIENTED_EDGE ( 'NONE', *, *, #365, .T. ) ;
#470=ADVANCED_FACE ( 'NONE', ( #3301 ), #3368, .F. ) ;
#471=CYLINDRICAL_SURFACE ( 'NONE', #3708, 0.7500000000000006661 ) ;
#472=ORIENTED_EDGE ( 'NONE', *, *, #741, .F. ) ;
#473=CARTESIAN_POINT ( 'NONE',  ( 14.24236788465317538, -1.151086274564850909, 28.47772737627938611 ) ) ;
#474=APPLICATION_CONTEXT ( 'automotive_design' ) ;
#475=DIRECTION ( 'NONE',  ( 0.000000000000000000, 1.000000000000000000, 0.000000000000000000 ) ) ;
#479=CARTESIAN_POINT ( 'NONE',  ( 7.620007234561953169, -3.569652013451328099, 31.86762445358909446 ) ) ;
#482=DIRECTION ( 'NONE',  ( -0.000000000000000000, -0.000000000000000000, 1.000000000000000000 ) ) ;
#485=ADVANCED_FACE ( 'NONE', ( #1868 ), #2298, .F. ) ;
#488=PLANE ( 'NONE',  #2053 ) ;
#489=ORIENTED_EDGE ( 'NONE', *, *, #4501, .T. ) ;
#493=CARTESIAN_POINT ( 'NONE',  ( 13.94789458910929980, 3.103566891827359786, 33.66190161997707975 ) ) ;
#498=LINE ( 'NONE', #2965, #2859 ) ;
#502=CIRCLE ( 'NONE', #4412, 0.7500000000000006661 ) ;
#503=CARTESIAN_POINT ( 'NONE',  ( -12.37116490068859775, 7.151597986548673624, 31.86762445358908735 ) ) ;
#509=CARTESIAN_POINT ( 'NONE',  ( 8.370007234561949616, -6.393402013451325416, 17.90262445358908039 ) ) ;
#513=CARTESIAN_POINT ( 'NONE',  ( 14.00286465610359699, 2.844890123102346013, 29.68689173443506490 ) ) ;
#516=CARTESIAN_POINT ( 'NONE',  ( 14.03294702938207017, -2.686088116544980586, 29.50362573057097748 ) ) ;
#522=VECTOR ( 'NONE', #2236, 1000.000000000000000 ) ;
#532=DIRECTION ( 'NONE',  ( 0.000000000000000000, 0.000000000000000000, 1.000000000000000000 ) ) ;
#535=DIRECTION ( 'NONE',  ( 0.000000000000000000, 0.000000000000000000, 1.000000000000000000 ) ) ;
#539=CARTESIAN_POINT ( 'NONE',  ( 12.37117936981251809, -7.143402013451325416, 17.79434398117761518 ) ) ;
#541=LINE ( 'NONE', #2628, #2266 ) ;
#543=ORIENTED_EDGE ( 'NONE', *, *, #3769, .F. ) ;
#546=CARTESIAN_POINT ( 'NONE',  ( 14.24247936672400172, 1.158380674401813248, 35.25801904860673375 ) ) ;
#552=CIRCLE ( 'NONE', #2205, 0.7500000000000006661 ) ;
#553=CARTESIAN_POINT ( 'NONE',  ( 5.708183634273623852, -3.565902013451327068, -1.469875546410923661 ) ) ;
#556=CARTESIAN_POINT ( 'NONE',  ( -14.12134633028087372, 2.185469490339439602, 34.70800415505340908 ) ) ;
#557=CARTESIAN_POINT ( 'NONE',  ( 12.37117936981252164, -7.143402013451325416, 17.90262445358908039 ) ) ;
#559=LINE ( 'NONE', #4518, #4646 ) ;
#560=VERTEX_POINT ( 'NONE', #3031 ) ;
#564=FACE_BOUND ( 'NONE', #2564, .T. ) ;
#567=VERTEX_POINT ( 'NONE', #2679 ) ;
#576=CARTESIAN_POINT ( 'NONE',  ( -14.28749276543804569, 0.004097986548671483757, 35.44137445358909133 ) ) ;
#577=DIRECTION ( 'NONE',  ( -1.000000000000000000, -0.000000000000000000, -0.000000000000000000 ) ) ;
#578=CIRCLE ( 'NONE', #4186, 0.7499999999999997780 ) ;
#580=CARTESIAN_POINT ( 'NONE',  ( -13.83947632439384812, -3.546053490249568618, 31.39589353661586557 ) ) ;
#586=VECTOR ( 'NONE', #1807, 1000.000000000000000 ) ;
#587=DIRECTION ( 'NONE',  ( 0.000000000000000000, -0.000000000000000000, -1.000000000000000000 ) ) ;
#590=FILL_AREA_STYLE_COLOUR ( '', #4459 ) ;
#593=ORIENTED_EDGE ( 'NONE', *, *, #2041, .F. ) ;
#594=DIRECTION ( 'NONE',  ( -1.000000000000000000, 1.076498916035107744E-16, 0.000000000000000000 ) ) ;
#608=ORIENTED_EDGE ( 'NONE', *, *, #1858, .F. ) ;
#609=AXIS2_PLACEMENT_3D ( 'NONE', #1952, #2354, #4060 ) ;
#613=CIRCLE ( 'NONE', #1794, 6.397499999999999964 ) ;
#614=ORIENTED_EDGE ( 'NONE', *, *, #2744, .F. ) ;
#618=ORIENTED_EDGE ( 'NONE', *, *, #1715, .F. ) ;
#621=( GEOMETRIC_REPRESENTATION_CONTEXT ( 3 ) GLOBAL_UNCERTAINTY_ASSIGNED_CONTEXT ( ( #4151 ) ) GLOBAL_UNIT_ASSIGNED_CONTEXT ( ( #3277, #2536, #4002 ) ) REPRESENTATION_CONTEXT ( 'NONE', 'WORKASPACE' ) );
#632=CARTESIAN_POINT ( 'NONE',  ( 7.234561953626996335E-06, 0.004097986548672528061, -8.542375546410942988 ) ) ;
#636=DIRECTION ( 'NONE',  ( -0.000000000000000000, -0.000000000000000000, 1.000000000000000000 ) ) ;
#637=CARTESIAN_POINT ( 'NONE',  ( 13.83333536583607781, -3.569652013451328543, 31.86762445358909446 ) ) ;
#641=FACE_OUTER_BOUND ( 'NONE', #1386, .T. ) ;
#644=ADVANCED_FACE ( 'NONE', ( #1639 ), #1439, .T. ) ;
#647=EDGE_CURVE ( 'NONE', #2212, #1270, #1398, .T. ) ;
#654=CARTESIAN_POINT ( 'NONE',  ( -11.90638390633376709, -7.893402013451320975, 17.15262445358908039 ) ) ;
#657=VERTEX_POINT ( 'NONE', #327 ) ;
#658=ORIENTED_EDGE ( 'NONE', *, *, #1152, .F. ) ;
#660=DIRECTION ( 'NONE',  ( 1.000000000000000000, 0.000000000000000000, 0.000000000000000000 ) ) ;
#661=AXIS2_PLACEMENT_3D ( 'NONE', #2914, #1638, #3650 ) ;
#663=CARTESIAN_POINT ( 'NONE',  ( -8.369992765438043492, 6.401597986548673624, 17.15262445358908039 ) ) ;
#665=LINE ( 'NONE', #4242, #2306 ) ;
#670=DIRECTION ( 'NONE',  ( 1.000000000000000000, 0.000000000000000000, 0.000000000000000000 ) ) ;
#674=CARTESIAN_POINT ( 'NONE',  ( -8.369992765438045268, -7.143402013451323640, 17.90262445358908039 ) ) ;
#675=VERTEX_POINT ( 'NONE', #984 ) ;
#676=CARTESIAN_POINT ( 'NONE',  ( 12.39929365807998884, -7.095336152118751016, 32.82105853334657297 ) ) ;
#681=AXIS2_PLACEMENT_3D ( 'NONE', #97, #142, #475 ) ;
#682=ORIENTED_EDGE ( 'NONE', *, *, #406, .T. ) ;
#684=ORIENTED_EDGE ( 'NONE', *, *, #1424, .T. ) ;
#686=CARTESIAN_POINT ( 'NONE',  ( -14.28749276543804925, 0.004097986548672528061, 28.29387445358909403 ) ) ;
#687=PRODUCT_CONTEXT ( 'NONE', #2013, 'mechanical' ) ;
#688=CARTESIAN_POINT ( 'NONE',  ( -3.152215195724335839, -3.565902013451327068, -8.542375546410942988 ) ) ;
#696=VERTEX_POINT ( 'NONE', #3528 ) ;
#697=CARTESIAN_POINT ( 'NONE',  ( 14.28750723456195537, 0.004097986548674278397, 39.01512445358908820 ) ) ;
#698=VECTOR ( 'NONE', #4638, 1000.000000000000000 ) ;
#703=B_SPLINE_CURVE_WITH_KNOTS ( 'NONE', 3,
 ( #932, #459, #2970, #2270, #1000, #1696, #291, #1716, #4604, #4244 ),
 .UNSPECIFIED., .F., .F.,
 ( 4, 2, 2, 2, 4 ),
 ( 0.000000000000000000, 0.0003199342119934979684, 0.0006398684239869959368, 0.0009598026359804939052, 0.001279736847973991874 ),
 .UNSPECIFIED. ) ;
#705=ORIENTED_EDGE ( 'NONE', *, *, #163, .F. ) ;
#709=CARTESIAN_POINT ( 'NONE',  ( 12.58215288272680255, 6.776360850858033302, 34.20015322194399232 ) ) ;
#714=CARTESIAN_POINT ( 'NONE',  ( -12.37116490068861197, -7.143402013451323640, 31.86762445358908735 ) ) ;
#715=DIRECTION ( 'NONE',  ( 0.000000000000000000, 0.000000000000000000, -1.000000000000000000 ) ) ;
#717=VECTOR ( 'NONE', #433, 1000.000000000000000 ) ;
#718=CARTESIAN_POINT ( 'NONE',  ( -14.28749276543804925, 0.004097986548672528061, 28.29387445358909403 ) ) ;
#725=CARTESIAN_POINT ( 'NONE',  ( -14.17127587220999274, 1.881159699106039751, 38.78036386370911970 ) ) ;
#727=ORIENTED_EDGE ( 'NONE', *, *, #1424, .F. ) ;
#728=VERTEX_POINT ( 'NONE', #674 ) ;
#733=CARTESIAN_POINT ( 'NONE',  ( -0.5650967372767217167, -3.565902013451328401, -9.700646504717855834 ) ) ;
#734=EDGE_CURVE ( 'NONE', #1942, #3678, #1058, .T. ) ;
#735=CARTESIAN_POINT ( 'NONE',  ( 8.370007234561949616, -7.143402013451325416, 17.90262445358908039 ) ) ;
#737=FACE_BOUND ( 'NONE', #3749, .T. ) ;
#738=FACE_BOUND ( 'NONE', #4116, .T. ) ;
#739=CARTESIAN_POINT ( 'NONE',  ( 13.83333536583607959, -3.569652013451329431, 32.10466053564423561 ) ) ;
#741=EDGE_CURVE ( 'NONE', #3225, #2052, #2478, .T. ) ;
#745=CARTESIAN_POINT ( 'NONE',  ( -13.83332089671217169, 3.577847986548673642, 31.86762445358909446 ) ) ;
#750=DIRECTION ( 'NONE',  ( 1.076498916035107744E-16, 1.000000000000000000, 0.000000000000000000 ) ) ;
#751=ORIENTED_EDGE ( 'NONE', *, *, #2927, .F. ) ;
#754=EDGE_LOOP ( 'NONE', ( #2143, #4391, #2842, #2593 ) ) ;
#755=ORIENTED_EDGE ( 'NONE', *, *, #3251, .T. ) ;
#757=CYLINDRICAL_SURFACE ( 'NONE', #1661, 14.28750000000000142 ) ;
#759=CARTESIAN_POINT ( 'NONE',  ( 14.16479288468515207, 1.886616767965749286, 38.76682706999739736 ) ) ;
#764=CARTESIAN_POINT ( 'NONE',  ( -14.00282210529756277, -2.836878008355436798, 34.04832179759813471 ) ) ;
#768=CARTESIAN_POINT ( 'NONE',  ( -14.28749276543804925, 0.004097986548672528061, 39.01512445358908820 ) ) ;
#769=ADVANCED_FACE ( 'NONE', ( #1985 ), #4591, .T. ) ;
#772=ORIENTED_EDGE ( 'NONE', *, *, #1281, .F. ) ;
#773=EDGE_CURVE ( 'NONE', #849, #4505, #1374, .T. ) ;
#775=CARTESIAN_POINT ( 'NONE',  ( -14.28749276543804925, 0.004097986548672528061, 39.01512445358908820 ) ) ;
#780=CARTESIAN_POINT ( 'NONE',  ( 14.09723484945316763, 2.339307409763772938, 38.62703793808391595 ) ) ;
#782=CARTESIAN_POINT ( 'NONE',  ( -8.369992765438038163, 7.151597986548673624, 31.86762445358908735 ) ) ;
#791=CARTESIAN_POINT ( 'NONE',  ( -12.87894808284510795, -6.188309651760397934, 35.46704985752301553 ) ) ;
#793=LINE ( 'NONE', #1935, #2576 ) ;
#794=EDGE_LOOP ( 'NONE', ( #3294, #1826, #3928, #916 ) ) ;
#801=ORIENTED_EDGE ( 'NONE', *, *, #3259, .T. ) ;
#802=ORIENTED_EDGE ( 'NONE', *, *, #395, .T. ) ;
#810=EDGE_CURVE ( 'NONE', #1644, #3603, #2778, .T. ) ;
#812=FACE_OUTER_BOUND ( 'NONE', #3133, .T. ) ;
#819=ORIENTED_EDGE ( 'NONE', *, *, #3769, .T. ) ;
#821=DIRECTION ( 'NONE',  ( 0.7071067811865449082, 0.000000000000000000, 0.7071067811865501263 ) ) ;
#822=CARTESIAN_POINT ( 'NONE',  ( 13.85858879626102791, 3.483479532322464323, 32.80720252877481613 ) ) ;
#824=ORIENTED_EDGE ( 'NONE', *, *, #1700, .T. ) ;
#826=AXIS2_PLACEMENT_3D ( 'NONE', #3565, #3822, #2806 ) ;
#827=DIRECTION ( 'NONE',  ( -1.000000000000000000, 1.076498916035107621E-16, -0.000000000000000000 ) ) ;
#831=PLANE ( 'NONE',  #985 ) ;
#833=CARTESIAN_POINT ( 'NONE',  ( 7.234561953626996335E-06, 0.004097986548672528061, -10.04237554641092345 ) ) ;
#837=EDGE_LOOP ( 'NONE', ( #1147, #281, #4283, #4594 ) ) ;
#840=CARTESIAN_POINT ( 'NONE',  ( 14.09176851988465629, 2.366970977748110716, 29.17628584082743259 ) ) ;
#843=FACE_OUTER_BOUND ( 'NONE', #264, .T. ) ;
#846=EDGE_CURVE ( 'NONE', #4649, #313, #2557, .T. ) ;
#847=CARTESIAN_POINT ( 'NONE',  ( 14.28750723456195537, 0.004097986548674313959, 35.44137445358909133 ) ) ;
#848=ADVANCED_FACE ( 'NONE', ( #812 ), #3681, .T. ) ;
#849=VERTEX_POINT ( 'NONE', #718 ) ;
#852=DIRECTION ( 'NONE',  ( -1.000000000000000000, 1.076498916035107744E-16, 0.000000000000000000 ) ) ;
#853=AXIS2_PLACEMENT_3D ( 'NONE', #2532, #750, #2185 ) ;
#860=CARTESIAN_POINT ( 'NONE',  ( -7.619992765438045268, 0.004097986548673348585, 31.86762445358909446 ) ) ;
#864=CARTESIAN_POINT ( 'NONE',  ( 12.37117936981252164, -7.143402013451325416, 17.90262445358908039 ) ) ;
#866=DIRECTION ( 'NONE',  ( 1.000000000000000000, 1.076498916035107621E-16, -0.000000000000000000 ) ) ;
#870=EDGE_CURVE ( 'NONE', #1869, #2259, #225, .T. ) ;
#871=EDGE_CURVE ( 'NONE', #313, #4140, #2012, .T. ) ;
#873=CARTESIAN_POINT ( 'NONE',  ( 14.25909360596529041, 0.9333857149738187253, 35.32631526480061979 ) ) ;
#878=DIRECTION ( 'NONE',  ( 0.000000000000000000, 1.000000000000000000, 0.000000000000000000 ) ) ;
#879=DIRECTION ( 'NONE',  ( 1.000000000000000000, -1.076498916035107621E-16, -0.000000000000000000 ) ) ;
#880=ORIENTED_EDGE ( 'NONE', *, *, #1621, .T. ) ;
#881=CARTESIAN_POINT ( 'NONE',  ( 8.370007234561953169, 7.151597986548671848, 31.86762445358908735 ) ) ;
#883=EDGE_CURVE ( 'NONE', #3060, #1630, #1523, .T. ) ;
#887=DIRECTION ( 'NONE',  ( 0.000000000000000000, 1.000000000000000000, 0.000000000000000000 ) ) ;
#889=ORIENTED_EDGE ( 'NONE', *, *, #2151, .F. ) ;
#891=CARTESIAN_POINT ( 'NONE',  ( 8.370007234561951392, 0.004097986548671627739, 31.86762445358908735 ) ) ;
#892=AXIS2_PLACEMENT_3D ( 'NONE', #3068, #4511, #4154 ) ;
#897=PLANE ( 'NONE',  #661 ) ;
#901=CARTESIAN_POINT ( 'NONE',  ( 14.99250723456195544, 7.901597986548669184, 17.90262445358908039 ) ) ;
#903=EDGE_LOOP ( 'NONE', ( #4589, #99, #2024, #2664 ) ) ;
#907=AXIS2_PLACEMENT_3D ( 'NONE', #255, #1703, #3238 ) ;
#908=ORIENTED_EDGE ( 'NONE', *, *, #3940, .T. ) ;
#910=CARTESIAN_POINT ( 'NONE',  ( 14.28750723456195537, 0.004097986548674313959, 35.44137445358909133 ) ) ;
#912=CARTESIAN_POINT ( 'NONE',  ( -14.03250527701334427, 2.696503014659202613, 34.22909654994315076 ) ) ;
#916=ORIENTED_EDGE ( 'NONE', *, *, #3259, .F. ) ;
#917=CYLINDRICAL_SURFACE ( 'NONE', #358, 3.573749999999999538 ) ;
#921=EDGE_LOOP ( 'NONE', ( #1969, #3596, #1759, #1916 ) ) ;
#923=EDGE_CURVE ( 'NONE', #675, #4505, #2472, .T. ) ;
#926=EDGE_LOOP ( 'NONE', ( #2588, #4099, #614, #3794, #1777, #942, #2345, #3510, #25, #928, #802, #3539, #3224, #2933, #1757, #1 ) ) ;
#928=ORIENTED_EDGE ( 'NONE', *, *, #286, .F. ) ;
#930=AXIS2_PLACEMENT_3D ( 'NONE', #2841, #1142, #4307 ) ;
#932=CARTESIAN_POINT ( 'NONE',  ( -12.37116490068861019, 7.151597986548670072, 17.90262445358908039 ) ) ;
#933=CARTESIAN_POINT ( 'NONE',  ( -13.87981558764485790, 3.394021350125140835, 33.02272327460092782 ) ) ;
#936=DIRECTION ( 'NONE',  ( 0.000000000000000000, 0.000000000000000000, -1.000000000000000000 ) ) ;
#940=EDGE_LOOP ( 'NONE', ( #1917, #3425, #308, #2711, #4407 ) ) ;
#942=ORIENTED_EDGE ( 'NONE', *, *, #923, .T. ) ;
#944=ADVANCED_FACE ( 'NONE', ( #2395 ), #1340, .T. ) ;
#947=ORIENTED_EDGE ( 'NONE', *, *, #1393, .F. ) ;
#949=DIRECTION ( 'NONE',  ( -1.000000000000000000, 1.076498916035107744E-16, 0.000000000000000000 ) ) ;
#954=LINE ( 'NONE', #553, #1501 ) ;
#957=ADVANCED_FACE ( 'NONE', ( #641 ), #2039, .F. ) ;
#963=EDGE_CURVE ( 'NONE', #98, #3102, #3083, .T. ) ;
#965=DIRECTION ( 'NONE',  ( 0.000000000000000000, 0.000000000000000000, -1.000000000000000000 ) ) ;
#967=AXIS2_PLACEMENT_3D ( 'NONE', #3873, #2228, #3272 ) ;
#968=ORIENTED_EDGE ( 'NONE', *, *, #3057, .F. ) ;
#970=DIRECTION ( 'NONE',  ( 0.000000000000000000, 0.000000000000000000, -1.000000000000000000 ) ) ;
#971=VERTEX_POINT ( 'NONE', #1412 ) ;
#973=CYLINDRICAL_SURFACE ( 'NONE', #2794, 3.573749999999999538 ) ;
#981=CARTESIAN_POINT ( 'NONE',  ( -6.869992765438046156, 6.401597986548673624, 17.15262445358908039 ) ) ;
#984=CARTESIAN_POINT ( 'NONE',  ( 14.28750723456195537, 0.004097986548674278397, 3.292624453589077405 ) ) ;
#985=AXIS2_PLACEMENT_3D ( 'NONE', #2268, #3703, #1179 ) ;
#991=ORIENTED_EDGE ( 'NONE', *, *, #2940, .F. ) ;
#995=EDGE_CURVE ( 'NONE', #4208, #4575, #3682, .T. ) ;
#996=EDGE_CURVE ( 'NONE', #1630, #3060, #2107, .T. ) ;
#997=ORIENTED_EDGE ( 'NONE', *, *, #2321, .F. ) ;
#1000=CARTESIAN_POINT ( 'NONE',  ( -12.27094482009613685, 7.322808560776099540, 17.41568789468882983 ) ) ;
#1001=DIRECTION ( 'NONE',  ( 1.000000000000000000, 0.000000000000000000, 0.000000000000000000 ) ) ;
#1002=CARTESIAN_POINT ( 'NONE',  ( 3.262507234561983438, 0.004097986548672528061, -10.04237554641092345 ) ) ;
#1003=CARTESIAN_POINT ( 'NONE',  ( -14.17571073093805545, -1.790345610955943467, 28.76824840355960333 ) ) ;
#1015=ORIENTED_EDGE ( 'NONE', *, *, #1490, .T. ) ;
#1020=ORIENTED_EDGE ( 'NONE', *, *, #3764, .F. ) ;
#1025=CARTESIAN_POINT ( 'NONE',  ( 7.234561953626996335E-06, 0.004097986548672528061, -8.542375546410942988 ) ) ;
#1030=CARTESIAN_POINT ( 'NONE',  ( 7.234561953626996335E-06, 0.004097986548672528061, 17.16762445358907385 ) ) ;
#1031=PRODUCT ( 'Part 131_Varsay\X2\0131\X0\lan', 'Part 131_Varsay\X2\0131\X0\lan', '', ( #687 ) ) ;
#1034=AXIS2_PLACEMENT_3D ( 'NONE', #1253, #2668, #887 ) ;
#1037=CARTESIAN_POINT ( 'NONE',  ( 12.37117936981252164, -7.143402013451326305, 31.86762445358908735 ) ) ;
#1041=ORIENTED_EDGE ( 'NONE', *, *, #2751, .T. ) ;
#1042=CARTESIAN_POINT ( 'NONE',  ( -12.62991449782762743, 6.684514975176426788, 34.41960495102418349 ) ) ;
#1049=CARTESIAN_POINT ( 'NONE',  ( 13.83082306713783538, 3.609921861597947590, 38.05633745867911699 ) ) ;
#1050=CIRCLE ( 'NONE', #3604, 1.499999999999999556 ) ;
#1055=DIRECTION ( 'NONE',  ( 1.000000000000000000, 0.000000000000000000, 0.000000000000000000 ) ) ;
#1056=CARTESIAN_POINT ( 'NONE',  ( 7.234561953626996335E-06, 0.004097986548672528061, 17.16762445358907385 ) ) ;
#1058=LINE ( 'NONE', #4253, #2928 ) ;
#1060=CARTESIAN_POINT ( 'NONE',  ( 14.28750723456195360, -0.4767427782355697641, 39.01512445358908820 ) ) ;
#1061=AXIS2_PLACEMENT_3D ( 'NONE', #346, #2877, #2834 ) ;
#1063=VECTOR ( 'NONE', #852, 1000.000000000000000 ) ;
#1067=CIRCLE ( 'NONE', #2633, 3.262500000000029932 ) ;
#1068=CARTESIAN_POINT ( 'NONE',  ( -13.23917829357126585, 5.378272323959379264, 36.58546145169297859 ) ) ;
#1073=CARTESIAN_POINT ( 'NONE',  ( -13.92246927997690520, 3.214374465122185942, 30.27987343953798671 ) ) ;
#1074=AXIS2_PLACEMENT_3D ( 'NONE', #891, #866, #3438 ) ;
#1080=LINE ( 'NONE', #3988, #3239 ) ;
#1081=DIRECTION ( 'NONE',  ( 0.000000000000000000, 0.000000000000000000, 1.000000000000000000 ) ) ;
#1082=DIRECTION ( 'NONE',  ( 0.000000000000000000, -1.000000000000000000, 0.000000000000000000 ) ) ;
#1089=ORIENTED_EDGE ( 'NONE', *, *, #4188, .F. ) ;
#1092=DIRECTION ( 'NONE',  ( 1.000000000000000000, 0.000000000000000000, 0.000000000000000000 ) ) ;
#1093=VERTEX_POINT ( 'NONE', #2503 ) ;
#1094=ORIENTED_EDGE ( 'NONE', *, *, #2618, .T. ) ;
#1095=CARTESIAN_POINT ( 'NONE',  ( -13.83332089671217346, 3.577847986548673642, 31.63353834203060089 ) ) ;
#1098=EDGE_CURVE ( 'NONE', #4620, #1844, #399, .T. ) ;
#1100=CARTESIAN_POINT ( 'NONE',  ( 13.42356499362135480, 4.900085295398275420, 37.07996709761046361 ) ) ;
#1103=EDGE_CURVE ( 'NONE', #4454, #1942, #2862, .T. ) ;
#1106=FACE_OUTER_BOUND ( 'NONE', #3904, .T. ) ;
#1108=CARTESIAN_POINT ( 'NONE',  ( 13.88012569863659884, -3.384623209710483138, 33.02628322023617358 ) ) ;
#1110=CARTESIAN_POINT ( 'NONE',  ( 14.28750723456195537, 0.004097986548674278397, 28.29387445358909403 ) ) ;
#1112=EDGE_LOOP ( 'NONE', ( #219, #1218, #682, #4622 ) ) ;
#1121=DIRECTION ( 'NONE',  ( 0.000000000000000000, 0.000000000000000000, 1.000000000000000000 ) ) ;
#1124=CARTESIAN_POINT ( 'NONE',  ( -14.25897937559747675, 0.9352445913789079190, 28.40934117879051257 ) ) ;
#1127=CARTESIAN_POINT ( 'NONE',  ( 1.403048712498150108, -3.565902013451326624, -9.476512138277032093 ) ) ;
#1133=DIRECTION ( 'NONE',  ( 0.000000000000000000, 0.000000000000000000, 1.000000000000000000 ) ) ;
#1134=CARTESIAN_POINT ( 'NONE',  ( 13.83333536583607781, -3.569652013451328543, 31.86762445358909446 ) ) ;
#1137=ADVANCED_FACE ( 'NONE', ( #1472 ), #3921, .T. ) ;
#1140=CARTESIAN_POINT ( 'NONE',  ( -14.05879861260986630, -2.551382414923340392, 38.54673083970037339 ) ) ;
#1142=DIRECTION ( 'NONE',  ( -1.000000000000000000, 1.076498916035107621E-16, 0.000000000000000000 ) ) ;
#1145=VECTOR ( 'NONE', #4634, 1000.000000000000000 ) ;
#1147=ORIENTED_EDGE ( 'NONE', *, *, #1715, .T. ) ;
#1152=EDGE_CURVE ( 'NONE', #2006, #3225, #541, .T. ) ;
#1154=AXIS2_PLACEMENT_3D ( 'NONE', #1652, #2715, #4156 ) ;
#1155=CARTESIAN_POINT ( 'NONE',  ( 3.152229664848242852, -3.565902013451327068, -8.542375546410942988 ) ) ;
#1157=DIRECTION ( 'NONE',  ( -0.000000000000000000, -0.000000000000000000, -1.000000000000000000 ) ) ;
#1160=DIRECTION ( 'NONE',  ( -1.076498916035107621E-16, -1.000000000000000000, 0.000000000000000000 ) ) ;
#1161=CARTESIAN_POINT ( 'NONE',  ( -12.37116490068861019, -7.893402013451320975, 17.15262445358908039 ) ) ;
#1165=CARTESIAN_POINT ( 'NONE',  ( -13.42355052449745578, -4.891889322300933429, 37.07996709761046361 ) ) ;
#1168=VERTEX_POINT ( 'NONE', #4469 ) ;
#1179=DIRECTION ( 'NONE',  ( 1.000000000000000000, 0.000000000000000000, -0.000000000000000000 ) ) ;
#1182=CARTESIAN_POINT ( 'NONE',  ( -14.28749276543804569, 0.004097986548671483757, 35.44137445358909133 ) ) ;
#1185=ORIENTED_EDGE ( 'NONE', *, *, #3877, .F. ) ;
#1188=CARTESIAN_POINT ( 'NONE',  ( -12.76961484722885665, -6.407663495538594489, 35.06035830646955276 ) ) ;
#1190=CARTESIAN_POINT ( 'NONE',  ( 14.12123733592186348, -2.178197668763618644, 29.02782019034563632 ) ) ;
#1191=CARTESIAN_POINT ( 'NONE',  ( -12.37116490068861019, 7.151597986548670072, 17.15262445358908039 ) ) ;
#1195=AXIS2_PLACEMENT_3D ( 'NONE', #2798, #2036, #660 ) ;
#1196=ORIENTED_EDGE ( 'NONE', *, *, #4290, .F. ) ;
#1201=CARTESIAN_POINT ( 'NONE',  ( 12.30672416701672134, 7.262191182741068118, 17.49673779855212885 ) ) ;
#1204=CARTESIAN_POINT ( 'NONE',  ( -14.00302738571292593, 2.844081521322073591, 34.04968199708700638 ) ) ;
#1206=DIRECTION ( 'NONE',  ( 1.000000000000000000, 0.000000000000000000, 0.000000000000000000 ) ) ;
#1209=ADVANCED_FACE ( 'NONE', ( #2652 ), #4498, .F. ) ;
#1211=CARTESIAN_POINT ( 'NONE',  ( 13.87971749024427304, 3.394489565583088453, 30.71374466332406783 ) ) ;
#1213=CARTESIAN_POINT ( 'NONE',  ( 13.87988322485530546, -3.385627302013072715, 30.71164830921944500 ) ) ;
#1215=LINE ( 'NONE', #1524, #522 ) ;
#1216=CARTESIAN_POINT ( 'NONE',  ( 14.03249099270719391, 2.696693369464580048, 34.22896506685294327 ) ) ;
#1217=ORIENTED_EDGE ( 'NONE', *, *, #2893, .F. ) ;
#1218=ORIENTED_EDGE ( 'NONE', *, *, #741, .T. ) ;
#1220=EDGE_CURVE ( 'NONE', #567, #3011, #4443, .T. ) ;
#1226=CARTESIAN_POINT ( 'NONE',  ( -14.25913809868193383, 0.9325616501008066050, 35.32655817869163428 ) ) ;
#1227=FACE_OUTER_BOUND ( 'NONE', #2626, .T. ) ;
#1231=ORIENTED_EDGE ( 'NONE', *, *, #883, .F. ) ;
#1236=LINE ( 'NONE', #2656, #1862 ) ;
#1244=DIRECTION ( 'NONE',  ( -1.355782318074878530E-16, -1.000000000000000000, 0.000000000000000000 ) ) ;
#1248=CARTESIAN_POINT ( 'NONE',  ( 11.96612007996801630, 7.811560636311104311, 17.15262445358908039 ) ) ;
#1249=ADVANCED_FACE ( 'NONE', ( #135 ), #488, .T. ) ;
#1253=CARTESIAN_POINT ( 'NONE',  ( 7.620007234561953169, 0.004097986548671708404, 31.86762445358909446 ) ) ;
#1257=CARTESIAN_POINT ( 'NONE',  ( 14.25899930818333239, 0.9350067622299832459, 28.40931988154160592 ) ) ;
#1261=FACE_OUTER_BOUND ( 'NONE', #2120, .T. ) ;
#1262=ORIENTED_EDGE ( 'NONE', *, *, #3466, .F. ) ;
#1264=CARTESIAN_POINT ( 'NONE',  ( 13.92222483456183291, 3.215475260645864086, 33.45288421949413760 ) ) ;
#1266=EDGE_LOOP ( 'NONE', ( #2501, #1728, #1991, #2164 ) ) ;
#1268=CIRCLE ( 'NONE', #3880, 0.7499999999999997780 ) ;
#1270=VERTEX_POINT ( 'NONE', #1932 ) ;
#1272=SHAPE_REPRESENTATION_RELATIONSHIP ( 'NONE' , 'NONE' ,  #3415, #2680 ) ;
#1275=CYLINDRICAL_SURFACE ( 'NONE', #609, 0.7499999999999997780 ) ;
#1277=ORIENTED_EDGE ( 'NONE', *, *, #1220, .T. ) ;
#1278=CARTESIAN_POINT ( 'NONE',  ( 12.13299545363123322, -7.541351341831832755, 17.23390984512910507 ) ) ;
#1280=AXIS2_PLACEMENT_3D ( 'NONE', #2732, #31, #2848 ) ;
#1281=EDGE_CURVE ( 'NONE', #1270, #971, #2811, .T. ) ;
#1289=ORIENTED_EDGE ( 'NONE', *, *, #1933, .T. ) ;
#1290=PLANE ( 'NONE',  #1678 ) ;
#1291=DIRECTION ( 'NONE',  ( 0.000000000000000000, -1.000000000000000000, 0.000000000000000000 ) ) ;
#1293=ORIENTED_EDGE ( 'NONE', *, *, #1753, .F. ) ;
#1298=DIRECTION ( 'NONE',  ( 1.000000000000000000, 0.000000000000000000, 0.000000000000000000 ) ) ;
#1301=CIRCLE ( 'NONE', #3088, 3.262500000000029932 ) ;
#1302=AXIS2_PLACEMENT_3D ( 'NONE', #4205, #4228, #2090 ) ;
#1304=CARTESIAN_POINT ( 'NONE',  ( -13.92260559306886236, -3.205595778353110159, 30.27860310428867052 ) ) ;
#1307=AXIS2_PLACEMENT_3D ( 'NONE', #367, #2832, #1812 ) ;
#1321=PLANE ( 'NONE',  #1280 ) ;
#1330=DIRECTION ( 'NONE',  ( 0.000000000000000000, 0.000000000000000000, 1.000000000000000000 ) ) ;
#1332=VERTEX_POINT ( 'NONE', #2070 ) ;
#1334=ORIENTED_EDGE ( 'NONE', *, *, #4082, .F. ) ;
#1340=CYLINDRICAL_SURFACE ( 'NONE', #3905, 4.762499999999999289 ) ;
#1342=CIRCLE ( 'NONE', #3654, 7.147499999999999076 ) ;
#1355=DIRECTION ( 'NONE',  ( -0.000000000000000000, -0.000000000000000000, -1.000000000000000000 ) ) ;
#1361=ORIENTED_EDGE ( 'NONE', *, *, #2467, .T. ) ;
#1362=DIRECTION ( 'NONE',  ( 1.000000000000000000, 0.000000000000000000, 0.000000000000000000 ) ) ;
#1370=CARTESIAN_POINT ( 'NONE',  ( -14.28749276543805102, -0.4634559803284261648, 28.29387445358910469 ) ) ;
#1374=LINE ( 'NONE', #3269, #3161 ) ;
#1377=VECTOR ( 'NONE', #297, 1000.000000000000000 ) ;
#1378=ORIENTED_EDGE ( 'NONE', *, *, #1734, .F. ) ;
#1379=CARTESIAN_POINT ( 'NONE',  ( 13.30085109409153787, -5.216069998034902788, 36.75526953962744159 ) ) ;
#1380=LINE ( 'NONE', #3831, #1418 ) ;
#1382=PRESENTATION_STYLE_ASSIGNMENT (( #3160 ) ) ;
#1384=EDGE_LOOP ( 'NONE', ( #4211, #727, #2317, #146 ) ) ;
#1385=CYLINDRICAL_SURFACE ( 'NONE', #3875, 4.762499999999999289 ) ;
#1386=EDGE_LOOP ( 'NONE', ( #1800, #3090, #991, #200 ) ) ;
#1392=AXIS2_PLACEMENT_3D ( 'NONE', #366, #2852, #3234 ) ;
#1393=EDGE_CURVE ( 'NONE', #3850, #254, #2923, .T. ) ;
#1396=CARTESIAN_POINT ( 'NONE',  ( 7.620007234561954057, -6.393402013451326305, 31.86762445358908735 ) ) ;
#1398=LINE ( 'NONE', #2837, #2710 ) ;
#1399=EDGE_LOOP ( 'NONE', ( #3181, #1941, #3245, #2347, #489, #3507, #2286, #4314, #997, #1690, #138, #1289 ) ) ;
#1400=CARTESIAN_POINT ( 'NONE',  ( 13.11669926372341344, -5.662485946417288751, 36.22991310522755981 ) ) ;
#1401=B_SPLINE_CURVE_WITH_KNOTS ( 'NONE', 3,
 ( #697, #1060, #1754, #4544, #3178, #4614, #4637, #4566, #3130, #4209, #3554, #1379, #278, #1400, #2482, #4187, #2074, #2815, #3830, #4279, #4256, #676, #1688, #1037 ),
 .UNSPECIFIED., .F., .F.,
 ( 4, 2, 2, 2, 2, 2, 2, 2, 2, 2, 2, 4 ),
 ( 0.01136174788562027173, 0.01278160237203083797, 0.01420145685844140422, 0.01562131134485196873, 0.01633123858805725359, 0.01704116583126253498, 0.01775109307446781637, 0.01846102031767310123, 0.01988087480408368135, 0.02059080204728896968, 0.02130072929049425801, 0.02272058377690481731 ),
 .UNSPECIFIED. ) ;
#1408=VERTEX_POINT ( 'NONE', #4274 ) ;
#1412=CARTESIAN_POINT ( 'NONE',  ( 7.620007234561954057, -6.393402013451325416, 17.90262445358908039 ) ) ;
#1414=AXIS2_PLACEMENT_3D ( 'NONE', #663, #3886, #4287 ) ;
#1418=VECTOR ( 'NONE', #1355, 1000.000000000000000 ) ;
#1424=EDGE_CURVE ( 'NONE', #2966, #3364, #2477, .T. ) ;
#1432=ORIENTED_EDGE ( 'NONE', *, *, #2584, .F. ) ;
#1435=VECTOR ( 'NONE', #3406, 1000.000000000000000 ) ;
#1439=CYLINDRICAL_SURFACE ( 'NONE', #1302, 3.573749999999999538 ) ;
#1440=EDGE_CURVE ( 'NONE', #1093, #1498, #2548, .T. ) ;
#1443=CARTESIAN_POINT ( 'NONE',  ( 12.39927133462508912, 7.103558341128515252, 32.81963905935650416 ) ) ;
#1445=CYLINDRICAL_SURFACE ( 'NONE', #930, 0.7500000000000006661 ) ;
#1446=DIRECTION ( 'NONE',  ( 0.000000000000000000, 0.000000000000000000, -1.000000000000000000 ) ) ;
#1447=ADVANCED_FACE ( 'NONE', ( #1814 ), #2106, .F. ) ;
#1451=CARTESIAN_POINT ( 'NONE',  ( -12.87886805896745201, 6.196644199065969971, 35.46669787887593372 ) ) ;
#1457=DIRECTION ( 'NONE',  ( 1.000000000000000000, 0.000000000000000000, 0.000000000000000000 ) ) ;
#1460=CARTESIAN_POINT ( 'NONE',  ( 13.05598868158019066, 5.808767766071424532, 36.04450365193367389 ) ) ;
#1462=DIRECTION ( 'NONE',  ( 0.000000000000000000, 0.000000000000000000, 1.000000000000000000 ) ) ;
#1463=DIRECTION ( 'NONE',  ( 1.000000000000000000, -1.076498916035107744E-16, -0.000000000000000000 ) ) ;
#1472=FACE_OUTER_BOUND ( 'NONE', #176, .T. ) ;
#1475=ORIENTED_EDGE ( 'NONE', *, *, #4216, .F. ) ;
#1476=CARTESIAN_POINT ( 'NONE',  ( -12.37116490068861019, 7.151597986548673624, 32.34872277302695665 ) ) ;
#1478=DIRECTION ( 'NONE',  ( 1.076498916035107621E-16, 1.000000000000000000, -0.000000000000000000 ) ) ;
#1480=CARTESIAN_POINT ( 'NONE',  ( 0.5742288748238882912, -3.565902013451327512, -9.691754032660345075 ) ) ;
#1484=PLANE ( 'NONE',  #2772 ) ;
#1487=AXIS2_PLACEMENT_3D ( 'NONE', #4545, #1330, #217 ) ;
#1490=EDGE_CURVE ( 'NONE', #2026, #1270, #149, .T. ) ;
#1491=CARTESIAN_POINT ( 'NONE',  ( -3.262492765438076869, 0.004097986548672927914, -10.04237554641092345 ) ) ;
#1492=ADVANCED_FACE ( 'NONE', ( #2922, #738 ), #1484, .F. ) ;
#1498=VERTEX_POINT ( 'NONE', #2203 ) ;
#1501=VECTOR ( 'NONE', #289, 1000.000000000000000 ) ;
#1502=CARTESIAN_POINT ( 'NONE',  ( 13.23943380891023480, 5.377675367566115305, 36.58613208551275164 ) ) ;
#1509=CARTESIAN_POINT ( 'NONE',  ( 14.03294734829104051, -2.686071323426693525, 34.23161090455447209 ) ) ;
#1513=VERTEX_POINT ( 'NONE', #3991 ) ;
#1516=EDGE_CURVE ( 'NONE', #657, #1093, #1050, .T. ) ;
#1518=AXIS2_PLACEMENT_3D ( 'NONE', #1789, #1082, #1446 ) ;
#1520=ORIENTED_EDGE ( 'NONE', *, *, #2887, .T. ) ;
#1523=CIRCLE ( 'NONE', #4139, 3.573749999999999538 ) ;
#1524=CARTESIAN_POINT ( 'NONE',  ( 12.37117936981252164, -7.143402013451325416, 17.15262445358908039 ) ) ;
#1534=CARTESIAN_POINT ( 'NONE',  ( 14.20084427493783430, -1.582011882117793089, 35.07860273982173993 ) ) ;
#1537=ADVANCED_FACE ( 'NONE', ( #1106 ), #2096, .F. ) ;
#1542=DIRECTION ( 'NONE',  ( -1.000000000000000000, 0.000000000000000000, 0.000000000000000000 ) ) ;
#1549=ORIENTED_EDGE ( 'NONE', *, *, #4501, .F. ) ;
#1553=CARTESIAN_POINT ( 'NONE',  ( 14.12144963474243298, -2.176777660462316799, 34.70846562849202144 ) ) ;
#1557=ORIENTED_EDGE ( 'NONE', *, *, #2983, .F. ) ;
#1558=CARTESIAN_POINT ( 'NONE',  ( 8.370007234561949616, -7.893402013451326305, 17.15262445358908039 ) ) ;
#1559=CIRCLE ( 'NONE', #3575, 1.499999999999999556 ) ;
#1560=CARTESIAN_POINT ( 'NONE',  ( -13.60390977449484318, -4.366406831334375127, 37.52789170789247208 ) ) ;
#1563=AXIS2_PLACEMENT_3D ( 'NONE', #3066, #594, #1672 ) ;
#1567=CARTESIAN_POINT ( 'NONE',  ( 7.620007234561953169, 0.004097986548671547075, 31.86762445358908735 ) ) ;
#1569=VERTEX_POINT ( 'NONE', #2223 ) ;
#1574=( NAMED_UNIT ( * ) SI_UNIT ( $, .STERADIAN. ) SOLID_ANGLE_UNIT ( ) );
#1576=CARTESIAN_POINT ( 'NONE',  ( -13.92217699914708895, 3.215616030937979541, 33.45254891481317117 ) ) ;
#1577=FACE_OUTER_BOUND ( 'NONE', #3371, .T. ) ;
#1586=CARTESIAN_POINT ( 'NONE',  ( 8.370007234561949616, 7.151597986548671848, 17.90262445358908039 ) ) ;
#1588=CARTESIAN_POINT ( 'NONE',  ( 14.12152400421957132, 2.184333436165076137, 34.70878884231233030 ) ) ;
#1603=CARTESIAN_POINT ( 'NONE',  ( 14.99250723456195544, 7.151597986548670072, 31.86762445358908735 ) ) ;
#1604=CARTESIAN_POINT ( 'NONE',  ( -7.619992765438044380, 6.401597986548673624, 17.90262445358908039 ) ) ;
#1605=ORIENTED_EDGE ( 'NONE', *, *, #2075, .F. ) ;
#1607=CARTESIAN_POINT ( 'NONE',  ( 13.92220696890103504, 3.215556595662160788, 30.28246602885027983 ) ) ;
#1608=CARTESIAN_POINT ( 'NONE',  ( -11.90638390633376531, 7.901597986548672736, 17.15262445358908039 ) ) ;
#1620=DIRECTION ( 'NONE',  ( 1.000000000000000000, -0.000000000000000000, 0.000000000000000000 ) ) ;
#1621=EDGE_CURVE ( 'NONE', #4543, #3471, #2995, .T. ) ;
#1623=VERTEX_POINT ( 'NONE', #1626 ) ;
#1625=EDGE_CURVE ( 'NONE', #560, #1840, #3672, .T. ) ;
#1626=CARTESIAN_POINT ( 'NONE',  ( -8.369992765438043492, 7.901597986548672736, 17.15262445358908039 ) ) ;
#1627=CARTESIAN_POINT ( 'NONE',  ( -13.86254354666967181, 3.463085079448043668, 32.79636359570053372 ) ) ;
#1628=LINE ( 'NONE', #462, #4446 ) ;
#1630=VERTEX_POINT ( 'NONE', #4058 ) ;
#1631=FACE_OUTER_BOUND ( 'NONE', #940, .T. ) ;
#1638=DIRECTION ( 'NONE',  ( 0.000000000000000000, 0.000000000000000000, 1.000000000000000000 ) ) ;
#1639=FACE_OUTER_BOUND ( 'NONE', #1266, .T. ) ;
#1641=ADVANCED_FACE ( 'NONE', ( #4131 ), #3354, .T. ) ;
#1644=VERTEX_POINT ( 'NONE', #910 ) ;
#1645=ORIENTED_EDGE ( 'NONE', *, *, #3929, .T. ) ;
#1650=CYLINDRICAL_SURFACE ( 'NONE', #1563, 3.573749999999999538 ) ;
#1651=CARTESIAN_POINT ( 'NONE',  ( -7.619992765438044380, 6.401597986548673624, 31.86762445358908735 ) ) ;
#1652=CARTESIAN_POINT ( 'NONE',  ( 14.99250723456195189, 0.004097986548670913901, 31.86762445358908735 ) ) ;
#1653=VECTOR ( 'NONE', #3024, 1000.000000000000000 ) ;
#1657=VERTEX_POINT ( 'NONE', #2334 ) ;
#1661=AXIS2_PLACEMENT_3D ( 'NONE', #407, #3957, #2829 ) ;
#1663=EDGE_CURVE ( 'NONE', #2259, #2212, #4050, .T. ) ;
#1665=CIRCLE ( 'NONE', #441, 0.7499999999999997780 ) ;
#1666=EDGE_CURVE ( 'NONE', #1168, #728, #2646, .T. ) ;
#1667=LINE ( 'NONE', #1491, #698 ) ;
#1670=CARTESIAN_POINT ( 'NONE',  ( -14.28749276543804925, 0.004097986548672528061, 17.15262445358908039 ) ) ;
#1671=ORIENTED_EDGE ( 'NONE', *, *, #3386, .T. ) ;
#1672=DIRECTION ( 'NONE',  ( 0.000000000000000000, -1.000000000000000000, 0.000000000000000000 ) ) ;
#1676=CARTESIAN_POINT ( 'NONE',  ( -14.17582932413400698, 1.797604608222738154, 34.96753936920406147 ) ) ;
#1678=AXIS2_PLACEMENT_3D ( 'NONE', #2301, #100, #3699 ) ;
#1688=CARTESIAN_POINT ( 'NONE',  ( 12.37117936981251809, -7.143402013451327193, 32.34872277302695665 ) ) ;
#1690=ORIENTED_EDGE ( 'NONE', *, *, #3764, .T. ) ;
#1692=LINE ( 'NONE', #1670, #3849 ) ;
#1696=CARTESIAN_POINT ( 'NONE',  ( -12.18356754445638934, 7.467360972742721259, 17.28331626890179606 ) ) ;
#1700=EDGE_CURVE ( 'NONE', #4499, #2486, #3753, .T. ) ;
#1702=CARTESIAN_POINT ( 'NONE',  ( 14.28750723456195537, 0.004097986548674278397, 17.15262445358908039 ) ) ;
#1703=DIRECTION ( 'NONE',  ( 0.000000000000000000, 1.000000000000000000, 0.000000000000000000 ) ) ;
#1704=ORIENTED_EDGE ( 'NONE', *, *, #2927, .T. ) ;
#1706=CARTESIAN_POINT ( 'NONE',  ( -8.369992765438045268, -7.143402013451325416, 31.86762445358908735 ) ) ;
#1711=FILL_AREA_STYLE ('',( #590 ) ) ;
#1715=EDGE_CURVE ( 'NONE', #3678, #4543, #1665, .T. ) ;
#1716=CARTESIAN_POINT ( 'NONE',  ( -12.02323085454684026, 7.723227117728908908, 17.16825211198572632 ) ) ;
#1723=ORIENTED_EDGE ( 'NONE', *, *, #365, .F. ) ;
#1727=FACE_OUTER_BOUND ( 'NONE', #2682, .T. ) ;
#1728=ORIENTED_EDGE ( 'NONE', *, *, #996, .T. ) ;
#1731=SURFACE_SIDE_STYLE ('',( #3135 ) ) ;
#1732=ADVANCED_FACE ( 'NONE', ( #3429 ), #203, .T. ) ;
#1734=EDGE_CURVE ( 'NONE', #2372, #3102, #703, .T. ) ;
#1735=ORIENTED_EDGE ( 'NONE', *, *, #883, .T. ) ;
#1746=CARTESIAN_POINT ( 'NONE',  ( 12.02324532367074639, -7.715031144631558035, 17.16825211198572632 ) ) ;
#1752=ORIENTED_EDGE ( 'NONE', *, *, #3349, .T. ) ;
#1753=EDGE_CURVE ( 'NONE', #3364, #4499, #2698, .T. ) ;
#1754=CARTESIAN_POINT ( 'NONE',  ( 14.26331614974113116, -0.9480807546542656672, 38.96710911585693538 ) ) ;
#1756=ORIENTED_EDGE ( 'NONE', *, *, #3734, .T. ) ;
#1757=ORIENTED_EDGE ( 'NONE', *, *, #3466, .T. ) ;
#1758=CARTESIAN_POINT ( 'NONE',  ( -12.37116490068859775, 7.151597986548673624, 31.86762445358908735 ) ) ;
#1759=ORIENTED_EDGE ( 'NONE', *, *, #647, .F. ) ;
#1762=LINE ( 'NONE', #385, #586 ) ;
#1765=CARTESIAN_POINT ( 'NONE',  ( 7.234561953626996335E-06, 0.004097986548672528061, 3.292624453589077405 ) ) ;
#1767=VECTOR ( 'NONE', #3192, 1000.000000000000000 ) ;
#1768=CARTESIAN_POINT ( 'NONE',  ( -8.369992765438045268, -7.143402013451325416, 31.86762445358908735 ) ) ;
#1772=CARTESIAN_POINT ( 'NONE',  ( 7.234561953626996335E-06, 0.004097986548672528061, 17.15262445358908039 ) ) ;
#1777=ORIENTED_EDGE ( 'NONE', *, *, #1980, .T. ) ;
#1789=CARTESIAN_POINT ( 'NONE',  ( 6.870007234561952281, 6.401597986548672736, 17.90262445358908039 ) ) ;
#1790=CIRCLE ( 'NONE', #1034, 3.573749999999999538 ) ;
#1794=AXIS2_PLACEMENT_3D ( 'NONE', #4458, #879, #1244 ) ;
#1800=ORIENTED_EDGE ( 'NONE', *, *, #251, .T. ) ;
#1807=DIRECTION ( 'NONE',  ( -1.076498916035107621E-16, -1.000000000000000000, 0.000000000000000000 ) ) ;
#1812=DIRECTION ( 'NONE',  ( -1.000000000000000000, 1.076498916035107744E-16, 0.000000000000000000 ) ) ;
#1814=FACE_OUTER_BOUND ( 'NONE', #4308, .T. ) ;
#1815=CARTESIAN_POINT ( 'NONE',  ( -13.92228970185832360, -3.206939127556818647, 33.45361016550401700 ) ) ;
#1816=DIRECTION ( 'NONE',  ( 1.000000000000000000, 0.000000000000000000, 0.000000000000000000 ) ) ;
#1821=CARTESIAN_POINT ( 'NONE',  ( 13.83333536583607959, 3.577847986548670978, 31.86762445358909446 ) ) ;
#1823=ORIENTED_EDGE ( 'NONE', *, *, #263, .F. ) ;
#1825=CARTESIAN_POINT ( 'NONE',  ( -12.51136670683754204, 6.903696596236023275, 33.74860486214563338 ) ) ;
#1826=ORIENTED_EDGE ( 'NONE', *, *, #1666, .T. ) ;
#1829=CARTESIAN_POINT ( 'NONE',  ( 13.66282301451940384, 4.187435799058254027, 37.66764907019537389 ) ) ;
#1833=DIRECTION ( 'NONE',  ( 1.000000000000000000, 1.076498916035107621E-16, -0.000000000000000000 ) ) ;
#1835=DIRECTION ( 'NONE',  ( 0.000000000000000000, 0.000000000000000000, 1.000000000000000000 ) ) ;
#1837=CARTESIAN_POINT ( 'NONE',  ( -14.20052575156873687, -1.584670739552391128, 35.07725914476921503 ) ) ;
#1839=CARTESIAN_POINT ( 'NONE',  ( 14.25916189650278199, -0.9246870515760209353, 28.40864894478323777 ) ) ;
#1840=VERTEX_POINT ( 'NONE', #3122 ) ;
#1844=VERTEX_POINT ( 'NONE', #4199 ) ;
#1848=CARTESIAN_POINT ( 'NONE',  ( -14.20092307528143216, 1.589399652140962127, 28.65623357306510854 ) ) ;
#1849=EDGE_CURVE ( 'NONE', #4, #1270, #4277, .T. ) ;
#1854=CARTESIAN_POINT ( 'NONE',  ( 7.620007234561951392, 6.401597986548672736, 31.86762445358908735 ) ) ;
#1855=EDGE_CURVE ( 'NONE', #3011, #1332, #2022, .T. ) ;
#1858=EDGE_CURVE ( 'NONE', #1623, #2437, #3303, .T. ) ;
#1860=CARTESIAN_POINT ( 'NONE',  ( -13.83332089671217169, -3.569652013451326322, 31.86762445358909446 ) ) ;
#1862=VECTOR ( 'NONE', #2981, 1000.000000000000000 ) ;
#1866=CARTESIAN_POINT ( 'NONE',  ( -13.23941933978631980, -5.369479394468771538, 36.58613208551273033 ) ) ;
#1868=FACE_OUTER_BOUND ( 'NONE', #2121, .T. ) ;
#1869=VERTEX_POINT ( 'NONE', #3457 ) ;
#1874=CARTESIAN_POINT ( 'NONE',  ( 0.1449758980921853624, -3.565902013451327068, -9.734783654012170828 ) ) ;
#1877=CARTESIAN_POINT ( 'NONE',  ( 12.18303796752544166, 7.468253174740091538, 17.28264009582345651 ) ) ;
#1879=AXIS2_PLACEMENT_3D ( 'NONE', #2449, #577, #2423 ) ;
#1881=CARTESIAN_POINT ( 'NONE',  ( 14.09186822061629663, -2.358077515305471827, 34.55938405561921201 ) ) ;
#1884=ORIENTED_EDGE ( 'NONE', *, *, #1625, .F. ) ;
#1896=ORIENTED_EDGE ( 'NONE', *, *, #4216, .T. ) ;
#1899=VERTEX_POINT ( 'NONE', #1002 ) ;
#1902=CARTESIAN_POINT ( 'NONE',  ( 14.28750723456195537, -0.2315532576940860787, 35.44137445358909133 ) ) ;
#1903=LINE ( 'NONE', #1997, #3009 ) ;
#1909=DIRECTION ( 'NONE',  ( 0.000000000000000000, -1.000000000000000000, 0.000000000000000000 ) ) ;
#1910=AXIS2_PLACEMENT_3D ( 'NONE', #632, #3509, #279 ) ;
#1912=CARTESIAN_POINT ( 'NONE',  ( 13.83333536583607604, -3.569652013451329875, 31.63041714010483219 ) ) ;
#1913=CARTESIAN_POINT ( 'NONE',  ( 12.37117936981251987, 7.151597986548670072, 31.86762445358908735 ) ) ;
#1915=DIRECTION ( 'NONE',  ( -1.000000000000000000, -1.076498916035107621E-16, 0.000000000000000000 ) ) ;
#1916=ORIENTED_EDGE ( 'NONE', *, *, #1663, .F. ) ;
#1917=ORIENTED_EDGE ( 'NONE', *, *, #2467, .F. ) ;
#1919=CARTESIAN_POINT ( 'NONE',  ( -12.13219254000220459, -7.542609400219328464, 17.23334239392281475 ) ) ;
#1925=CARTESIAN_POINT ( 'NONE',  ( -13.94750378805149360, 3.105294744008160635, 33.65912111070095136 ) ) ;
#1926=FACE_OUTER_BOUND ( 'NONE', #2444, .T. ) ;
#1932=CARTESIAN_POINT ( 'NONE',  ( 7.620007234561951392, 6.401597986548672736, 17.90262445358908039 ) ) ;
#1933=EDGE_CURVE ( 'NONE', #657, #3907, #4374, .T. ) ;
#1935=CARTESIAN_POINT ( 'NONE',  ( -4.762492765438045339, 0.004097986548673111795, -10.04237554641092345 ) ) ;
#1937=CARTESIAN_POINT ( 'NONE',  ( -6.869992765438044380, 12.08996809382683857, 17.90262445358908039 ) ) ;
#1938=ADVANCED_FACE ( 'NONE', ( #1926 ), #2336, .F. ) ;
#1940=CIRCLE ( 'NONE', #207, 14.28750000000000142 ) ;
#1941=ORIENTED_EDGE ( 'NONE', *, *, #163, .T. ) ;
#1942=VERTEX_POINT ( 'NONE', #1604 ) ;
#1945=CARTESIAN_POINT ( 'NONE',  ( -12.37116490068861552, -7.143402013451322752, 17.79394892777614601 ) ) ;
#1950=DIRECTION ( 'NONE',  ( 1.000000000000000000, 0.000000000000000000, 0.000000000000000000 ) ) ;
#1952=CARTESIAN_POINT ( 'NONE',  ( -8.369992765438043492, 6.401597986548673624, 3.292624453589077405 ) ) ;
#1953=DIRECTION ( 'NONE',  ( 1.000000000000000000, 0.000000000000000000, 0.000000000000000000 ) ) ;
#1956=CARTESIAN_POINT ( 'NONE',  ( 14.28155886016486598, 0.4760400057381644068, 28.31745088146499967 ) ) ;
#1962=ADVANCED_FACE ( 'NONE', ( #1577 ), #1976, .T. ) ;
#1967=ORIENTED_EDGE ( 'NONE', *, *, #3940, .F. ) ;
#1969=ORIENTED_EDGE ( 'NONE', *, *, #2066, .F. ) ;
#1972=EDGE_LOOP ( 'NONE', ( #2357, #1671 ) ) ;
#1976=CYLINDRICAL_SURFACE ( 'NONE', #3838, 3.573749999999999538 ) ;
#1979=CARTESIAN_POINT ( 'NONE',  ( 12.35746789565908799, -7.167253453071094960, 17.68815867240257589 ) ) ;
#1980=EDGE_CURVE ( 'NONE', #567, #675, #2290, .T. ) ;
#1981=ORIENTED_EDGE ( 'NONE', *, *, #647, .T. ) ;
#1985=FACE_OUTER_BOUND ( 'NONE', #837, .T. ) ;
#1991=ORIENTED_EDGE ( 'NONE', *, *, #3877, .T. ) ;
#1996=DIRECTION ( 'NONE',  ( -1.000000000000000000, 0.000000000000000000, 0.000000000000000000 ) ) ;
#1997=CARTESIAN_POINT ( 'NONE',  ( 8.370007234561949616, 7.151597986548671848, 31.86762445358908735 ) ) ;
#2002=CARTESIAN_POINT ( 'NONE',  ( 12.18358201358030080, -7.459164999645373939, 17.28331626890179606 ) ) ;
#2004=ORIENTED_EDGE ( 'NONE', *, *, #406, .F. ) ;
#2005=CARTESIAN_POINT ( 'NONE',  ( -17.48249276543803532, -7.143402013451320975, 3.292624453589076960 ) ) ;
#2006=VERTEX_POINT ( 'NONE', #182 ) ;
#2007=CIRCLE ( 'NONE', #3202, 4.762499999999999289 ) ;
#2009=DIRECTION ( 'NONE',  ( -1.000000000000000000, 0.000000000000000000, 0.000000000000000000 ) ) ;
#2012=B_SPLINE_CURVE_WITH_KNOTS ( 'NONE', 3,
 ( #576, #3355, #3754, #1226, #3430, #2647, #1676, #556, #181, #912, #1204, #1925, #1576, #933, #1627, #131, #3018, #4059 ),
 .UNSPECIFIED., .F., .F.,
 ( 4, 2, 2, 2, 2, 2, 2, 2, 4 ),
 ( 1.014745470810651806E-18, 0.0007013035162779033670, 0.001402607032555805867, 0.002103910548833708150, 0.002805214065111610432, 0.003506517581389512715, 0.004207821097667415432, 0.004909124613945317281, 0.005610428130223219997 ),
 .UNSPECIFIED. ) ;
#2013=APPLICATION_CONTEXT ( 'automotive_design' ) ;
#2015=CIRCLE ( 'NONE', #4642, 0.7500000000000006661 ) ;
#2022=LINE ( 'NONE', #2807, #4353 ) ;
#2024=ORIENTED_EDGE ( 'NONE', *, *, #4082, .T. ) ;
#2025=DIRECTION ( 'NONE',  ( 0.000000000000000000, 0.000000000000000000, -1.000000000000000000 ) ) ;
#2026=VERTEX_POINT ( 'NONE', #3044 ) ;
#2029=ORIENTED_EDGE ( 'NONE', *, *, #1753, .T. ) ;
#2031=VECTOR ( 'NONE', #3042, 1000.000000000000000 ) ;
#2035=ADVANCED_FACE ( 'NONE', ( #1227 ), #1275, .T. ) ;
#2036=DIRECTION ( 'NONE',  ( -0.000000000000000000, -0.000000000000000000, -1.000000000000000000 ) ) ;
#2039=TOROIDAL_SURFACE ( 'NONE', #4285, 1.500000000000000000, 0.7500000000000000000 ) ;
#2041=EDGE_CURVE ( 'NONE', #3102, #1623, #1628, .T. ) ;
#2042=DIRECTION ( 'NONE',  ( 0.000000000000000000, 0.000000000000000000, 1.000000000000000000 ) ) ;
#2045=CARTESIAN_POINT ( 'NONE',  ( -14.28749276543804925, 0.004097986548672528061, 28.29387445358909403 ) ) ;
#2052=VERTEX_POINT ( 'NONE', #557 ) ;
#2053=AXIS2_PLACEMENT_3D ( 'NONE', #2005, #3001, #4422 ) ;
#2065=DIRECTION ( 'NONE',  ( 0.000000000000000000, 0.000000000000000000, 1.000000000000000000 ) ) ;
#2066=EDGE_CURVE ( 'NONE', #4, #2259, #1903, .T. ) ;
#2070=CARTESIAN_POINT ( 'NONE',  ( 7.620007234561953169, 3.577847986548671422, 31.86762445358909446 ) ) ;
#2074=CARTESIAN_POINT ( 'NONE',  ( 12.76995131259341498, -6.406996766056419546, 35.06135232679011438 ) ) ;
#2075=EDGE_CURVE ( 'NONE', #1899, #1408, #1301, .T. ) ;
#2077=DIRECTION ( 'NONE',  ( 0.000000000000000000, 0.000000000000000000, 1.000000000000000000 ) ) ;
#2085=DIRECTION ( 'NONE',  ( 1.000000000000000000, 0.000000000000000000, 0.000000000000000000 ) ) ;
#2087=DIRECTION ( 'NONE',  ( -0.000000000000000000, -0.000000000000000000, 1.000000000000000000 ) ) ;
#2090=DIRECTION ( 'NONE',  ( -1.000000000000000000, 0.000000000000000000, 0.000000000000000000 ) ) ;
#2092=DIRECTION ( 'NONE',  ( 1.000000000000000000, 0.000000000000000000, 0.000000000000000000 ) ) ;
#2096=TOROIDAL_SURFACE ( 'NONE', #3461, 1.500000000000000000, 0.7500000000000000000 ) ;
#2097=CARTESIAN_POINT ( 'NONE',  ( -14.28749276543804569, 0.004097986548671483757, 35.44137445358909133 ) ) ;
#2101=ORIENTED_EDGE ( 'NONE', *, *, #4428, .F. ) ;
#2106=TOROIDAL_SURFACE ( 'NONE', #2179, 1.500000000000000000, 0.7500000000000000000 ) ;
#2107=CIRCLE ( 'NONE', #2253, 3.573749999999999538 ) ;
#2108=CYLINDRICAL_SURFACE ( 'NONE', #2115, 14.28750000000000142 ) ;
#2115=AXIS2_PLACEMENT_3D ( 'NONE', #2920, #1157, #2149 ) ;
#2116=ORIENTED_EDGE ( 'NONE', *, *, #2744, .T. ) ;
#2120=EDGE_LOOP ( 'NONE', ( #1723, #2169 ) ) ;
#2121=EDGE_LOOP ( 'NONE', ( #1262, #140, #755, #1475 ) ) ;
#2133=DIRECTION ( 'NONE',  ( 0.000000000000000000, 0.000000000000000000, 1.000000000000000000 ) ) ;
#2140=ORIENTED_EDGE ( 'NONE', *, *, #1663, .T. ) ;
#2143=ORIENTED_EDGE ( 'NONE', *, *, #114, .T. ) ;
#2144=FACE_OUTER_BOUND ( 'NONE', #4550, .T. ) ;
#2145=LINE ( 'NONE', #3582, #2908 ) ;
#2148=CARTESIAN_POINT ( 'NONE',  ( 13.60392424361874575, 4.374602804431722447, 37.52789170789245787 ) ) ;
#2149=DIRECTION ( 'NONE',  ( -1.000000000000000000, 0.000000000000000000, 0.000000000000000000 ) ) ;
#2151=EDGE_CURVE ( 'NONE', #1840, #4649, #2663, .T. ) ;
#2164=ORIENTED_EDGE ( 'NONE', *, *, #1393, .T. ) ;
#2166=CARTESIAN_POINT ( 'NONE',  ( -13.48424197071718567, 4.730921210558564738, 37.23391125615017927 ) ) ;
#2168=ADVANCED_FACE ( 'NONE', ( #4101 ), #1290, .F. ) ;
#2169=ORIENTED_EDGE ( 'NONE', *, *, #923, .F. ) ;
#2170=FACE_OUTER_BOUND ( 'NONE', #926, .T. ) ;
#2173=CARTESIAN_POINT ( 'NONE',  ( 13.11703699520739441, 5.669897148686642296, 36.23092228855527708 ) ) ;
#2174=EDGE_CURVE ( 'NONE', #2259, #2006, #236, .T. ) ;
#2177=DIRECTION ( 'NONE',  ( -1.000000000000000000, 0.000000000000000000, 0.000000000000000000 ) ) ;
#2178=CARTESIAN_POINT ( 'NONE',  ( -7.619992765438044380, 12.08996809382683857, 39.01512445358908110 ) ) ;
#2179=AXIS2_PLACEMENT_3D ( 'NONE', #3942, #1133, #3308 ) ;
#2180=CARTESIAN_POINT ( 'NONE',  ( -13.94746062085793881, -3.097275023406871775, 33.65873331764755250 ) ) ;
#2183=DIRECTION ( 'NONE',  ( 1.000000000000000000, -0.000000000000000000, -0.000000000000000000 ) ) ;
#2184=CARTESIAN_POINT ( 'NONE',  ( -13.05597421245628098, -5.800571792974073659, 36.04450365193367389 ) ) ;
#2185=DIRECTION ( 'NONE',  ( -1.000000000000000000, 1.076498916035107744E-16, 0.000000000000000000 ) ) ;
#2198=CARTESIAN_POINT ( 'NONE',  ( 14.28750723456195537, 0.4850620214986993139, 39.01512445358908820 ) ) ;
#2203=CARTESIAN_POINT ( 'NONE',  ( -7.619992765438047044, -6.393402013451324528, 17.90262445358908039 ) ) ;
#2204=CARTESIAN_POINT ( 'NONE',  ( -13.83934412749958121, -3.546568056405964064, 32.33580404679898379 ) ) ;
#2205=AXIS2_PLACEMENT_3D ( 'NONE', #306, #2386, #970 ) ;
#2210=CARTESIAN_POINT ( 'NONE',  ( -4.762492765438045339, 0.004097986548673111795, -8.542375546410942988 ) ) ;
#2212=VERTEX_POINT ( 'NONE', #1854 ) ;
#2214=CARTESIAN_POINT ( 'NONE',  ( -12.58714829887031073, 6.764457034226218468, 34.20002532364928527 ) ) ;
#2220=CIRCLE ( 'NONE', #2436, 0.7500000000000006661 ) ;
#2223=CARTESIAN_POINT ( 'NONE',  ( 12.37117936981251987, 7.151597986548668295, 17.90262445358908039 ) ) ;
#2227=VERTEX_POINT ( 'NONE', #201 ) ;
#2228=DIRECTION ( 'NONE',  ( 0.000000000000000000, 0.000000000000000000, 1.000000000000000000 ) ) ;
#2236=DIRECTION ( 'NONE',  ( 0.000000000000000000, 0.000000000000000000, 1.000000000000000000 ) ) ;
#2237=ORIENTED_EDGE ( 'NONE', *, *, #4567, .F. ) ;
#2242=ADVANCED_FACE ( 'NONE', ( #2689 ), #1650, .F. ) ;
#2247=DIRECTION ( 'NONE',  ( 0.000000000000000000, 0.000000000000000000, 1.000000000000000000 ) ) ;
#2248=CARTESIAN_POINT ( 'NONE',  ( 13.86272605794495405, -3.454216419310585540, 32.79868223278693762 ) ) ;
#2252=CARTESIAN_POINT ( 'NONE',  ( -13.93157240826945475, -3.195140614832279624, 38.27608545593862033 ) ) ;
#2253=AXIS2_PLACEMENT_3D ( 'NONE', #1056, #715, #2177 ) ;
#2254=ORIENTED_EDGE ( 'NONE', *, *, #2471, .T. ) ;
#2255=CARTESIAN_POINT ( 'NONE',  ( -8.369992765438043492, 7.151597986548673624, 17.90262445358908039 ) ) ;
#2259=VERTEX_POINT ( 'NONE', #881 ) ;
#2266=VECTOR ( 'NONE', #4065, 1000.000000000000000 ) ;
#2268=CARTESIAN_POINT ( 'NONE',  ( 7.234561953626996335E-06, 0.004097986548672528061, 17.15262445358908039 ) ) ;
#2270=CARTESIAN_POINT ( 'NONE',  ( -12.30737424917090195, 7.261058540042763632, 17.49889617799752983 ) ) ;
#2274=ORIENTED_EDGE ( 'NONE', *, *, #4608, .F. ) ;
#2275=DIRECTION ( 'NONE',  ( 9.517981353260378315E-33, 8.841607930564763213E-17, -1.000000000000000000 ) ) ;
#2276=CARTESIAN_POINT ( 'NONE',  ( 13.83944209648124080, 3.554443468061219580, 31.39667678951239083 ) ) ;
#2281=CARTESIAN_POINT ( 'NONE',  ( 3.262507234561983438, 0.004097986548672528061, -10.04237554641092345 ) ) ;
#2286=ORIENTED_EDGE ( 'NONE', *, *, #963, .T. ) ;
#2287=CARTESIAN_POINT ( 'NONE',  ( 12.02320382733283743, 7.723282363347554913, 17.16832378532597758 ) ) ;
#2290=LINE ( 'NONE', #3431, #3543 ) ;
#2293=DIRECTION ( 'NONE',  ( -1.000000000000000000, 1.076498916035107744E-16, 0.000000000000000000 ) ) ;
#2296=CARTESIAN_POINT ( 'NONE',  ( 13.86256790811323469, -3.454845676089625339, 30.93920252718416819 ) ) ;
#2298=CYLINDRICAL_SURFACE ( 'NONE', #681, 0.7500000000000006661 ) ;
#2301=CARTESIAN_POINT ( 'NONE',  ( 7.234561953626996335E-06, -3.565902013451327068, -1.469875546410923661 ) ) ;
#2306=VECTOR ( 'NONE', #1478, 1000.000000000000000 ) ;
#2315=DIRECTION ( 'NONE',  ( -1.000000000000000000, 1.076498916035107744E-16, -0.000000000000000000 ) ) ;
#2317=ORIENTED_EDGE ( 'NONE', *, *, #3658, .F. ) ;
#2321=EDGE_CURVE ( 'NONE', #4454, #1623, #4257, .T. ) ;
#2322=ORIENTED_EDGE ( 'NONE', *, *, #260, .T. ) ;
#2330=B_SPLINE_CURVE_WITH_KNOTS ( 'NONE', 3,
 ( #2045, #1370, #2786, #4224, #1003, #208, #3074, #3867, #3525, #4516, #1304, #2718, #4160, #580, #3459, #227 ),
 .UNSPECIFIED., .F., .F.,
 ( 4, 2, 2, 2, 2, 2, 2, 4 ),
 ( 0.01121786453620356172, 0.01261999568898472708, 0.01332106126537531063, 0.01402212684176589418, 0.01472319241815647772, 0.01542425799454706301, 0.01612532357093764482, 0.01682638914732823010 ),
 .UNSPECIFIED. ) ;
#2334=CARTESIAN_POINT ( 'NONE',  ( 8.370007234561949616, 7.901597986548672736, 17.15262445358908039 ) ) ;
#2336=PLANE ( 'NONE',  #2634 ) ;
#2338=DIRECTION ( 'NONE',  ( 0.000000000000000000, 1.000000000000000000, 0.000000000000000000 ) ) ;
#2339=ORIENTED_EDGE ( 'NONE', *, *, #810, .F. ) ;
#2345=ORIENTED_EDGE ( 'NONE', *, *, #773, .F. ) ;
#2347=ORIENTED_EDGE ( 'NONE', *, *, #3428, .T. ) ;
#2354=DIRECTION ( 'NONE',  ( 0.000000000000000000, -0.000000000000000000, 1.000000000000000000 ) ) ;
#2357=ORIENTED_EDGE ( 'NONE', *, *, #2075, .T. ) ;
#2367=EDGE_LOOP ( 'NONE', ( #1231, #3132 ) ) ;
#2372=VERTEX_POINT ( 'NONE', #74 ) ;
#2383=ORIENTED_EDGE ( 'NONE', *, *, #1098, .T. ) ;
#2386=DIRECTION ( 'NONE',  ( 0.000000000000000000, -1.000000000000000000, 0.000000000000000000 ) ) ;
#2390=CARTESIAN_POINT ( 'NONE',  ( -3.152215195724335839, -3.565902013451327068, -8.542375546410942988 ) ) ;
#2391=ADVANCED_FACE ( 'NONE', ( #2144 ), #3322, .F. ) ;
#2395=FACE_OUTER_BOUND ( 'NONE', #3275, .T. ) ;
#2400=ADVANCED_FACE ( 'NONE', ( #2775 ), #1385, .T. ) ;
#2405=ORIENTED_EDGE ( 'NONE', *, *, #1440, .T. ) ;
#2410=ADVANCED_FACE ( 'NONE', ( #843 ), #3715, .F. ) ;
#2414=ORIENTED_EDGE ( 'NONE', *, *, #1281, .T. ) ;
#2421=DIRECTION ( 'NONE',  ( -1.000000000000000000, 1.776412614630121196E-15, 0.000000000000000000 ) ) ;
#2423=DIRECTION ( 'NONE',  ( 0.000000000000000000, 0.000000000000000000, 1.000000000000000000 ) ) ;
#2429=ORIENTED_EDGE ( 'NONE', *, *, #1855, .T. ) ;
#2433=CARTESIAN_POINT ( 'NONE',  ( 7.234561953626996335E-06, 0.004097986548672528061, 17.15262445358908039 ) ) ;
#2434=CARTESIAN_POINT ( 'NONE',  ( 8.370007234561953169, -6.393402013451326305, 31.86762445358908735 ) ) ;
#2436=AXIS2_PLACEMENT_3D ( 'NONE', #4537, #2025, #3101 ) ;
#2437=VERTEX_POINT ( 'NONE', #2255 ) ;
#2444=EDGE_LOOP ( 'NONE', ( #4386, #2274 ) ) ;
#2445=CARTESIAN_POINT ( 'NONE',  ( -13.86271173127319400, 3.462410270568636150, 30.93674631171511180 ) ) ;
#2449=CARTESIAN_POINT ( 'NONE',  ( -8.369992765438043492, 7.901597986548672736, 17.90262445358908039 ) ) ;
#2451=LINE ( 'NONE', #252, #460 ) ;
#2460=EDGE_LOOP ( 'NONE', ( #947, #3606 ) ) ;
#2461=B_SPLINE_CURVE_WITH_KNOTS ( 'NONE', 3,
 ( #775, #380, #2844, #725, #2865, #4359, #2823, #2487, #3227, #2166, #2565, #4310, #1068, #2, #3930, #1451, #3605, #1042, #2214, #1825, #3646, #27, #1476, #1758 ),
 .UNSPECIFIED., .F., .F.,
 ( 4, 2, 2, 2, 2, 2, 2, 2, 2, 2, 2, 4 ),
 ( -1.301042606982605321E-18, 0.001420502804142392784, 0.002841005608284786869, 0.004261508412427179870, 0.004971759814498384611, 0.005682011216569587617, 0.006392262618640790622, 0.007102514020711995363, 0.008523016824854413517, 0.009233268226925623462, 0.009943519628996833407, 0.01136402243313923421 ),
 .UNSPECIFIED. ) ;
#2463=AXIS2_PLACEMENT_3D ( 'NONE', #4270, #2737, #4581 ) ;
#2466=CARTESIAN_POINT ( 'NONE',  ( -13.83947098521712249, 3.554273134874391005, 31.39569820401975164 ) ) ;
#2467=EDGE_CURVE ( 'NONE', #560, #4140, #1236, .T. ) ;
#2471=EDGE_CURVE ( 'NONE', #3603, #567, #2696, .T. ) ;
#2472=CIRCLE ( 'NONE', #451, 14.28750000000000142 ) ;
#2474=LINE ( 'NONE', #11, #3992 ) ;
#2477=LINE ( 'NONE', #3569, #4588 ) ;
#2478=LINE ( 'NONE', #300, #1145 ) ;
#2482=CARTESIAN_POINT ( 'NONE',  ( 13.05555083129287652, -5.801549086471636585, 36.04312068514320799 ) ) ;
#2486=VERTEX_POINT ( 'NONE', #2525 ) ;
#2487=CARTESIAN_POINT ( 'NONE',  ( -13.66251858288074850, 4.188395861520828767, 37.66696981337766914 ) ) ;
#2497=DIRECTION ( 'NONE',  ( -1.076498916035107621E-16, 1.000000000000000000, -0.000000000000000000 ) ) ;
#2500=DIRECTION ( 'NONE',  ( -1.000000000000000000, 1.076498916035107744E-16, 0.000000000000000000 ) ) ;
#2501=ORIENTED_EDGE ( 'NONE', *, *, #4196, .F. ) ;
#2503=CARTESIAN_POINT ( 'NONE',  ( -6.869992765438047932, -6.393402013451324528, 17.15262445358908039 ) ) ;
#2514=AXIS2_PLACEMENT_3D ( 'NONE', #2572, #1833, #3568 ) ;
#2517=CARTESIAN_POINT ( 'NONE',  ( 14.26329643125615476, 0.9577320989239291871, 38.96707689327597279 ) ) ;
#2520=CARTESIAN_POINT ( 'NONE',  ( 3.152229664848242852, -3.565902013451327068, -8.542375546410942988 ) ) ;
#2521=CARTESIAN_POINT ( 'NONE',  ( 4.762507234561953240, 0.004097986548672528061, -8.542375546410942988 ) ) ;
#2524=CARTESIAN_POINT ( 'NONE',  ( 14.24237798928296783, -1.151061070837056777, 35.25757041514634693 ) ) ;
#2525=CARTESIAN_POINT ( 'NONE',  ( 4.762507234561953240, 0.004097986548672528061, 3.292624453589077405 ) ) ;
#2532=CARTESIAN_POINT ( 'NONE',  ( 14.99250723456195544, 7.151597986548670072, 3.292624453589077405 ) ) ;
#2536=( NAMED_UNIT ( * ) PLANE_ANGLE_UNIT ( ) SI_UNIT ( $, .RADIAN. ) );
#2538=ORIENTED_EDGE ( 'NONE', *, *, #734, .T. ) ;
#2539=DIRECTION ( 'NONE',  ( 0.000000000000000000, 0.000000000000000000, 1.000000000000000000 ) ) ;
#2541=CARTESIAN_POINT ( 'NONE',  ( 2.193906090638697570, -3.565902013451327068, -9.141961161702393923 ) ) ;
#2544=FACE_OUTER_BOUND ( 'NONE', #921, .T. ) ;
#2548=CIRCLE ( 'NONE', #907, 0.7500000000000006661 ) ;
#2553=AXIS2_PLACEMENT_3D ( 'NONE', #3147, #3617, #1160 ) ;
#2556=CARTESIAN_POINT ( 'NONE',  ( -14.19372362644966756, -1.646721693147197740, 38.82591248395577566 ) ) ;
#2557=B_SPLINE_CURVE_WITH_KNOTS ( 'NONE', 3,
 ( #1860, #4037, #2204, #2948, #4416, #1815, #2180, #764, #392, #2574, #370, #4014, #1837, #3637, #4395, #3335, #435, #1182 ),
 .UNSPECIFIED., .F., .F.,
 ( 4, 2, 2, 2, 2, 2, 2, 2, 4 ),
 ( 0.01682638914732823010, 0.01752717873359116094, 0.01822796831985409177, 0.01892875790611702261, 0.01962954749237995344, 0.02033033707864288775, 0.02103112666490581859, 0.02173191625116874942, 0.02243270583743168026 ),
 .UNSPECIFIED. ) ;
#2559=B_SPLINE_CURVE_WITH_KNOTS ( 'NONE', 3,
 ( #4461, #1248, #2287, #2595, #1877, #3352, #1201, #3040, #2644, #151 ),
 .UNSPECIFIED., .F., .F.,
 ( 4, 2, 2, 2, 4 ),
 ( 0.000000000000000000, 0.0003186827706029870567, 0.0006373655412059741135, 0.0009560483118089611702, 0.001274731082411948227 ),
 .UNSPECIFIED. ) ;
#2560=EDGE_CURVE ( 'NONE', #2910, #4543, #1342, .T. ) ;
#2563=ORIENTED_EDGE ( 'NONE', *, *, #2954, .F. ) ;
#2564=EDGE_LOOP ( 'NONE', ( #3607, #968 ) ) ;
#2565=CARTESIAN_POINT ( 'NONE',  ( -13.42336662775846889, 4.900590130444159698, 37.07949484329716938 ) ) ;
#2570=CARTESIAN_POINT ( 'NONE',  ( 13.30106093516862842, 5.223730645347358426, 36.75583910459432246 ) ) ;
#2572=CARTESIAN_POINT ( 'NONE',  ( 7.620007234561951392, 12.08996809382683857, 39.01512445358908110 ) ) ;
#2573=DIRECTION ( 'NONE',  ( -1.000000000000000000, 1.076498916035107621E-16, 0.000000000000000000 ) ) ;
#2574=CARTESIAN_POINT ( 'NONE',  ( -14.09151203141540520, -2.360106401758869321, 34.55760183291916121 ) ) ;
#2575=DIRECTION ( 'NONE',  ( -1.000000000000000000, 1.076498916035107621E-16, -0.000000000000000000 ) ) ;
#2576=VECTOR ( 'NONE', #4470, 1000.000000000000000 ) ;
#2579=DIRECTION ( 'NONE',  ( 0.000000000000000000, 0.000000000000000000, 1.000000000000000000 ) ) ;
#2580=CARTESIAN_POINT ( 'NONE',  ( -13.83080859801392570, -3.601725888500601602, 38.05633745867910278 ) ) ;
#2584=EDGE_CURVE ( 'NONE', #3907, #696, #1940, .T. ) ;
#2585=DIRECTION ( 'NONE',  ( 0.000000000000000000, 0.000000000000000000, 1.000000000000000000 ) ) ;
#2588=ORIENTED_EDGE ( 'NONE', *, *, #57, .T. ) ;
#2593=ORIENTED_EDGE ( 'NONE', *, *, #1621, .F. ) ;
#2595=CARTESIAN_POINT ( 'NONE',  ( 12.13220700912610894, 7.550805373316674007, 17.23334239392282186 ) ) ;
#2600=ORIENTED_EDGE ( 'NONE', *, *, #1849, .F. ) ;
#2602=CONICAL_SURFACE ( 'NONE', #1487, 3.262500000000029932, 0.7853981633974446153 ) ;
#2604=CIRCLE ( 'NONE', #4034, 3.573749999999999538 ) ;
#2609=VECTOR ( 'NONE', #2315, 1000.000000000000000 ) ;
#2613=VERTEX_POINT ( 'NONE', #4515 ) ;
#2615=CONICAL_SURFACE ( 'NONE', #892, 3.262500000000029932, 0.7853981633974446153 ) ;
#2616=CARTESIAN_POINT ( 'NONE',  ( -12.37116490068861197, -7.143402013451321864, 17.90262445358908039 ) ) ;
#2618=EDGE_CURVE ( 'NONE', #971, #3225, #502, .T. ) ;
#2620=AXIS2_PLACEMENT_3D ( 'NONE', #1025, #2042, #2421 ) ;
#2622=DIRECTION ( 'NONE',  ( 1.000000000000000000, -1.076498916035107621E-16, -0.000000000000000000 ) ) ;
#2626=EDGE_LOOP ( 'NONE', ( #3787, #4019, #618, #3834 ) ) ;
#2627=CYLINDRICAL_SURFACE ( 'NONE', #4419, 0.7499999999999997780 ) ;
#2628=CARTESIAN_POINT ( 'NONE',  ( 8.370007234561949616, -7.143402013451325416, 17.15262445358908039 ) ) ;
#2633=AXIS2_PLACEMENT_3D ( 'NONE', #3588, #3548, #3193 ) ;
#2634=AXIS2_PLACEMENT_3D ( 'NONE', #132, #535, #3728 ) ;
#2635=B_SPLINE_CURVE_WITH_KNOTS ( 'NONE', 3,
 ( #121, #143, #822, #1264, #493, #3325, #1216, #4453, #1588, #3768, #2636, #546, #873, #2960, #3743, #847 ),
 .UNSPECIFIED., .F., .F.,
 ( 4, 2, 2, 2, 2, 2, 2, 4 ),
 ( 0.01121777374642162275, 0.01261988060185674498, 0.01332093402957430610, 0.01402198745729186721, 0.01472304088500942833, 0.01542409431272698944, 0.01612514774044455229, 0.01682620116816211167 ),
 .UNSPECIFIED. ) ;
#2636=CARTESIAN_POINT ( 'NONE',  ( 14.20053099622510118, 1.593282007777887976, 35.07724096963458749 ) ) ;
#2644=CARTESIAN_POINT ( 'NONE',  ( 12.37117936981252342, 7.151597986548670960, 17.79394892777614601 ) ) ;
#2645=CARTESIAN_POINT ( 'NONE',  ( 12.37117936981252164, -7.143402013451326305, 31.86762445358908735 ) ) ;
#2646=LINE ( 'NONE', #106, #2031 ) ;
#2647=CARTESIAN_POINT ( 'NONE',  ( -14.20057006193529858, 1.592637804043315564, 35.07746567129901649 ) ) ;
#2648=DIRECTION ( 'NONE',  ( -0.000000000000000000, -0.000000000000000000, -1.000000000000000000 ) ) ;
#2651=DIRECTION ( 'NONE',  ( 0.000000000000000000, -1.000000000000000000, 0.000000000000000000 ) ) ;
#2652=FACE_OUTER_BOUND ( 'NONE', #211, .T. ) ;
#2653=CARTESIAN_POINT ( 'NONE',  ( -17.48249276543803532, -7.893402013451320975, 17.90262445358908039 ) ) ;
#2656=CARTESIAN_POINT ( 'NONE',  ( 18.74250723456195189, 3.577847986548670534, 31.86762445358909446 ) ) ;
#2659=EDGE_CURVE ( 'NONE', #2437, #1942, #578, .T. ) ;
#2663=LINE ( 'NONE', #4053, #1063 ) ;
#2664=ORIENTED_EDGE ( 'NONE', *, *, #1666, .F. ) ;
#2665=CARTESIAN_POINT ( 'NONE',  ( 4.762507234561953240, 0.004097986548672528061, -10.04237554641092345 ) ) ;
#2668=DIRECTION ( 'NONE',  ( -1.000000000000000000, -1.076498916035107621E-16, 0.000000000000000000 ) ) ;
#2672=CARTESIAN_POINT ( 'NONE',  ( 14.03228452734540177, 2.697812684413582573, 29.50746059750024486 ) ) ;
#2674=ORIENTED_EDGE ( 'NONE', *, *, #57, .F. ) ;
#2676=EDGE_CURVE ( 'NONE', #1332, #116, #1790, .T. ) ;
#2677=PRODUCT_DEFINITION_CONTEXT ( 'detailed design', #474, 'design' ) ;
#2679=CARTESIAN_POINT ( 'NONE',  ( 14.28750723456195537, 0.004097986548674278397, 28.29387445358909403 ) ) ;
#2680=ADVANCED_BREP_SHAPE_REPRESENTATION ( '', ( #363, #4483 ), #4021 ) ;
#2682=EDGE_LOOP ( 'NONE', ( #1196, #1094, #658, #4282 ) ) ;
#2689=FACE_OUTER_BOUND ( 'NONE', #3208, .T. ) ;
#2692=CARTESIAN_POINT ( 'NONE',  ( -8.369992765438043492, 6.401597986548673624, 31.86762445358908735 ) ) ;
#2696=B_SPLINE_CURVE_WITH_KNOTS ( 'NONE', 3,
 ( #3028, #1912, #4472, #2296, #1213, #2956, #117, #4425, #516, #3738, #1190, #3343, #3691, #473, #1839, #2926, #4376, #1110 ),
 .UNSPECIFIED., .F., .F.,
 ( 4, 2, 2, 2, 2, 2, 2, 2, 4 ),
 ( 0.000000000000000000, 0.0007012932024186013802, 0.001402586404837202760, 0.002103879607255804141, 0.002805172809674405521, 0.003506466012093006901, 0.004207759214511608281, 0.004909052416930209661, 0.005610345619348811042 ),
 .UNSPECIFIED. ) ;
#2698=CIRCLE ( 'NONE', #2620, 4.762499999999999289 ) ;
#2699=CARTESIAN_POINT ( 'NONE',  ( -8.369992765438045268, -6.393402013451322752, 3.292624453589076960 ) ) ;
#2701=EDGE_CURVE ( 'NONE', #2006, #4636, #447, .T. ) ;
#2710=VECTOR ( 'NONE', #3920, 1000.000000000000000 ) ;
#2711=ORIENTED_EDGE ( 'NONE', *, *, #846, .T. ) ;
#2715=DIRECTION ( 'NONE',  ( -1.000000000000000000, 1.076498916035107744E-16, 0.000000000000000000 ) ) ;
#2718=CARTESIAN_POINT ( 'NONE',  ( -13.87970196760993069, -3.386323001426799539, 30.71342844021988938 ) ) ;
#2725=AXIS2_PLACEMENT_3D ( 'NONE', #3574, #3249, #24 ) ;
#2732=CARTESIAN_POINT ( 'NONE',  ( -17.48249276543803532, -7.143402013451320975, 3.292624453589076960 ) ) ;
#2737=DIRECTION ( 'NONE',  ( 0.000000000000000000, 0.000000000000000000, 1.000000000000000000 ) ) ;
#2740=DIRECTION ( 'NONE',  ( 1.076498916035107621E-16, -1.000000000000000000, 0.000000000000000000 ) ) ;
#2744=EDGE_CURVE ( 'NONE', #3011, #1644, #2635, .T. ) ;
#2748=ORIENTED_EDGE ( 'NONE', *, *, #773, .T. ) ;
#2751=EDGE_CURVE ( 'NONE', #4494, #2212, #128, .T. ) ;
#2759=DIRECTION ( 'NONE',  ( -1.000000000000000000, 1.076498916035107744E-16, 0.000000000000000000 ) ) ;
#2761=PLANE ( 'NONE',  #3616 ) ;
#2768=VECTOR ( 'NONE', #821, 1000.000000000000000 ) ;
#2772=AXIS2_PLACEMENT_3D ( 'NONE', #2178, #2573, #3218 ) ;
#2775=FACE_OUTER_BOUND ( 'NONE', #4165, .T. ) ;
#2776=DIRECTION ( 'NONE',  ( -1.000000000000000000, 1.076498916035107744E-16, 0.000000000000000000 ) ) ;
#2778=B_SPLINE_CURVE_WITH_KNOTS ( 'NONE', 3,
 ( #3240, #1902, #2879, #414, #2524, #1534, #3967, #1553, #1881, #1509, #3660, #2971, #4323, #1108, #2248, #2924, #739, #1134 ),
 .UNSPECIFIED., .F., .F.,
 ( 4, 2, 2, 2, 2, 2, 2, 2, 4 ),
 ( 0.01682620116816211167, 0.01752698813223788760, 0.01822777509631366005, 0.01892856206038943251, 0.01962934902446520843, 0.02033013598854098089, 0.02103092295261675682, 0.02173170991669252927, 0.02243249688076830173 ),
 .UNSPECIFIED. ) ;
#2786=CARTESIAN_POINT ( 'NONE',  ( -14.26312048591866599, -0.9355300642538868505, 28.38824789321300912 ) ) ;
#2787=LINE ( 'NONE', #1396, #3965 ) ;
#2791=CARTESIAN_POINT ( 'NONE',  ( 7.234561953626996335E-06, 0.004097986548672528061, 3.292624453589077405 ) ) ;
#2794=AXIS2_PLACEMENT_3D ( 'NONE', #220, #949, #1291 ) ;
#2795=ORIENTED_EDGE ( 'NONE', *, *, #2887, .F. ) ;
#2798=CARTESIAN_POINT ( 'NONE',  ( -8.369992765438045268, -6.393402013451324528, 17.90262445358908039 ) ) ;
#2800=ORIENTED_EDGE ( 'NONE', *, *, #183, .T. ) ;
#2806=DIRECTION ( 'NONE',  ( 1.000000000000000000, 0.000000000000000000, 0.000000000000000000 ) ) ;
#2807=CARTESIAN_POINT ( 'NONE',  ( 18.74250723456195189, 3.577847986548670534, 31.86762445358909446 ) ) ;
#2808=CYLINDRICAL_SURFACE ( 'NONE', #1392, 0.7499999999999997780 ) ;
#2810=LINE ( 'NONE', #1702, #3950 ) ;
#2811=LINE ( 'NONE', #3896, #3324 ) ;
#2815=CARTESIAN_POINT ( 'NONE',  ( 12.62992896695153178, -6.676319002079077691, 34.41960495102417639 ) ) ;
#2821=EDGE_CURVE ( 'NONE', #4620, #1168, #1380, .T. ) ;
#2823=CARTESIAN_POINT ( 'NONE',  ( -13.83077811249668976, 3.610099873504223122, 38.05628366828691611 ) ) ;
#2829=DIRECTION ( 'NONE',  ( -1.000000000000000000, 0.000000000000000000, 0.000000000000000000 ) ) ;
#2832=DIRECTION ( 'NONE',  ( 1.076498916035107744E-16, 1.000000000000000000, 0.000000000000000000 ) ) ;
#2833=CARTESIAN_POINT ( 'NONE',  ( -3.152215195724335839, -3.565902013451327068, -1.469875546410923661 ) ) ;
#2834=DIRECTION ( 'NONE',  ( 1.000000000000000000, 0.000000000000000000, 0.000000000000000000 ) ) ;
#2837=CARTESIAN_POINT ( 'NONE',  ( 7.620007234561951392, 6.401597986548672736, 17.15262445358908039 ) ) ;
#2841=CARTESIAN_POINT ( 'NONE',  ( -17.48249276543803532, -7.893402013451320975, 17.90262445358908039 ) ) ;
#2842=ORIENTED_EDGE ( 'NONE', *, *, #20, .T. ) ;
#2844=CARTESIAN_POINT ( 'NONE',  ( -14.26330168061722148, 0.9562767277516133202, 38.96710911585693538 ) ) ;
#2848=DIRECTION ( 'NONE',  ( 1.000000000000000000, -1.076498916035107621E-16, 0.000000000000000000 ) ) ;
#2850=CARTESIAN_POINT ( 'NONE',  ( 13.93158687739336088, 3.203336587929628720, 38.27608545593859901 ) ) ;
#2852=DIRECTION ( 'NONE',  ( -0.000000000000000000, 0.000000000000000000, -1.000000000000000000 ) ) ;
#2854=DIRECTION ( 'NONE',  ( 1.000000000000000000, 0.000000000000000000, 0.000000000000000000 ) ) ;
#2859=VECTOR ( 'NONE', #4030, 1000.000000000000000 ) ;
#2861=FACE_OUTER_BOUND ( 'NONE', #754, .T. ) ;
#2862=CIRCLE ( 'NONE', #243, 0.7500000000000006661 ) ;
#2865=CARTESIAN_POINT ( 'NONE',  ( -14.10221755691438972, 2.339333233612962193, 38.63906452781715473 ) ) ;
#2873=CIRCLE ( 'NONE', #2725, 3.573749999999999538 ) ;
#2877=DIRECTION ( 'NONE',  ( -0.000000000000000000, -0.000000000000000000, -1.000000000000000000 ) ) ;
#2879=CARTESIAN_POINT ( 'NONE',  ( 14.28168262043153725, -0.4640750791195977776, 35.41829268623339289 ) ) ;
#2887=EDGE_CURVE ( 'NONE', #4499, #3035, #3732, .T. ) ;
#2890=CARTESIAN_POINT ( 'NONE',  ( -13.83332089671217169, 3.577847986548673642, 31.86762445358909446 ) ) ;
#2893=EDGE_CURVE ( 'NONE', #2006, #4494, #1268, .T. ) ;
#2896=CARTESIAN_POINT ( 'NONE',  ( 0.2894426067789017121, -3.565902013451327512, -9.725952605682453012 ) ) ;
#2907=CARTESIAN_POINT ( 'NONE',  ( 3.152229664848242852, -3.565902013451327068, -1.469875546410923661 ) ) ;
#2908=VECTOR ( 'NONE', #5, 1000.000000000000000 ) ;
#2909=ORIENTED_EDGE ( 'NONE', *, *, #4276, .F. ) ;
#2910=VERTEX_POINT ( 'NONE', #1706 ) ;
#2914=CARTESIAN_POINT ( 'NONE',  ( 7.234561953626996335E-06, 0.004097986548672528061, 3.292624453589077405 ) ) ;
#2919=ADVANCED_FACE ( 'NONE', ( #261 ), #2602, .T. ) ;
#2920=CARTESIAN_POINT ( 'NONE',  ( 7.234561953626996335E-06, 0.004097986548672528061, 17.15262445358908039 ) ) ;
#2922=FACE_OUTER_BOUND ( 'NONE', #4517, .T. ) ;
#2923=CIRCLE ( 'NONE', #4362, 3.573749999999999538 ) ;
#2924=CARTESIAN_POINT ( 'NONE',  ( 13.83942910803283688, -3.546298317252753574, 32.33825509850257873 ) ) ;
#2926=CARTESIAN_POINT ( 'NONE',  ( 14.28175077624798739, -0.4627368126066581655, 28.31667831377500377 ) ) ;
#2927=EDGE_CURVE ( 'NONE', #3035, #338, #4639, .T. ) ;
#2928=VECTOR ( 'NONE', #3570, 1000.000000000000000 ) ;
#2929=ORIENTED_EDGE ( 'NONE', *, *, #4345, .T. ) ;
#2931=CARTESIAN_POINT ( 'NONE',  ( -12.39925686550117945, -7.095362368031173261, 32.81963905935649706 ) ) ;
#2933=ORIENTED_EDGE ( 'NONE', *, *, #963, .F. ) ;
#2940=EDGE_CURVE ( 'NONE', #4575, #971, #552, .T. ) ;
#2943=ORIENTED_EDGE ( 'NONE', *, *, #4290, .T. ) ;
#2944=FACE_BOUND ( 'NONE', #2460, .T. ) ;
#2946=ADVANCED_FACE ( 'NONE', ( #1727 ), #4235, .T. ) ;
#2948=CARTESIAN_POINT ( 'NONE',  ( -13.86245741347044103, -3.455229889388735209, 32.79470164932398291 ) ) ;
#2953=CARTESIAN_POINT ( 'NONE',  ( -14.09722038032925617, -2.331111436666425618, 38.62703793808391595 ) ) ;
#2954=EDGE_CURVE ( 'NONE', #1408, #3035, #1667, .T. ) ;
#2956=CARTESIAN_POINT ( 'NONE',  ( 13.92256690490806115, -3.205812800917074767, 30.27923183374419125 ) ) ;
#2960=CARTESIAN_POINT ( 'NONE',  ( 14.28155410871526065, 0.4758380746309069931, 35.41777643611839466 ) ) ;
#2963=ORIENTED_EDGE ( 'NONE', *, *, #1700, .F. ) ;
#2964=DIRECTION ( 'NONE',  ( 1.000000000000000000, 1.076498916035107621E-16, -0.000000000000000000 ) ) ;
#2965=CARTESIAN_POINT ( 'NONE',  ( -8.369992765438043492, 7.151597986548673624, 17.15262445358908039 ) ) ;
#2966=VERTEX_POINT ( 'NONE', #2907 ) ;
#2970=CARTESIAN_POINT ( 'NONE',  ( -12.35745342653517653, 7.175449426168442280, 17.68815867240257589 ) ) ;
#2971=CARTESIAN_POINT ( 'NONE',  ( 13.94778318531167471, -3.095894809702069761, 33.66111732484789343 ) ) ;
#2973=DIRECTION ( 'NONE',  ( 0.000000000000000000, 0.000000000000000000, 1.000000000000000000 ) ) ;
#2976=DIRECTION ( 'NONE',  ( -1.000000000000000000, 1.076498916035107744E-16, 0.000000000000000000 ) ) ;
#2981=DIRECTION ( 'NONE',  ( -1.000000000000000000, 1.076498916035107744E-16, 0.000000000000000000 ) ) ;
#2983=EDGE_CURVE ( 'NONE', #116, #1332, #2873, .T. ) ;
#2990=ORIENTED_EDGE ( 'NONE', *, *, #1516, .T. ) ;
#2993=( LENGTH_UNIT ( ) NAMED_UNIT ( * ) SI_UNIT ( .MILLI., .METRE. ) );
#2995=LINE ( 'NONE', #3334, #1435 ) ;
#2996=CARTESIAN_POINT ( 'NONE',  ( 7.234561953626996335E-06, 0.004097986548672528061, 17.16762445358907385 ) ) ;
#2997=DIRECTION ( 'NONE',  ( 0.000000000000000000, 0.000000000000000000, -1.000000000000000000 ) ) ;
#3001=DIRECTION ( 'NONE',  ( -1.076498916035107621E-16, -1.000000000000000000, -8.841607930564763213E-17 ) ) ;
#3002=ADVANCED_FACE ( 'NONE', ( #3901 ), #1445, .F. ) ;
#3009=VECTOR ( 'NONE', #4087, 1000.000000000000000 ) ;
#3010=ORIENTED_EDGE ( 'NONE', *, *, #2066, .T. ) ;
#3011=VERTEX_POINT ( 'NONE', #1821 ) ;
#3017=DIRECTION ( 'NONE',  ( -1.000000000000000000, 0.000000000000000000, -0.000000000000000000 ) ) ;
#3018=CARTESIAN_POINT ( 'NONE',  ( -13.83332089671217524, 3.577847986548674086, 32.10183545663884530 ) ) ;
#3024=DIRECTION ( 'NONE',  ( -1.000000000000000000, 1.076498916035107744E-16, -0.000000000000000000 ) ) ;
#3025=CARTESIAN_POINT ( 'NONE',  ( 13.83333536583607959, 3.577847986548671422, 31.63389550438917297 ) ) ;
#3028=CARTESIAN_POINT ( 'NONE',  ( 13.83333536583607781, -3.569652013451328543, 31.86762445358909446 ) ) ;
#3030=LINE ( 'NONE', #1191, #4482 ) ;
#3031=CARTESIAN_POINT ( 'NONE',  ( -7.619992765438045268, 3.577847986548672754, 31.86762445358909446 ) ) ;
#3035=VERTEX_POINT ( 'NONE', #2210 ) ;
#3037=DIRECTION ( 'NONE',  ( 0.000000000000000000, 0.000000000000000000, -1.000000000000000000 ) ) ;
#3038=ORIENTED_EDGE ( 'NONE', *, *, #1858, .T. ) ;
#3040=CARTESIAN_POINT ( 'NONE',  ( 12.35764476757788621, 7.175150426935585912, 17.68847735315404535 ) ) ;
#3042=DIRECTION ( 'NONE',  ( 1.000000000000000000, -1.076498916035107621E-16, 0.000000000000000000 ) ) ;
#3044=CARTESIAN_POINT ( 'NONE',  ( 6.870007234561952281, 6.401597986548672736, 17.15262445358908039 ) ) ;
#3046=CLOSED_SHELL ( 'NONE', ( #3700, #2400, #1962, #2242, #1209, #3736, #3854, #3375, #1492, #4542, #3512, #1732, #3395, #3049, #848, #3725, #1249, #328, #4152, #2035, #470, #769, #1537, #4223, #2410, #1447, #3002, #3176, #1137, #2946, #3114, #957, #2391, #4003, #485, #644, #3314, #944, #1641, #2919, #1938, #2168 ) ) ;
#3049=ADVANCED_FACE ( 'NONE', ( #2861 ), #47, .T. ) ;
#3056=LINE ( 'NONE', #3390, #3666 ) ;
#3057=EDGE_CURVE ( 'NONE', #2613, #2486, #4389, .T. ) ;
#3060=VERTEX_POINT ( 'NONE', #4616 ) ;
#3066=CARTESIAN_POINT ( 'NONE',  ( 18.74250723456195189, 0.004097986548670510577, 31.86762445358909446 ) ) ;
#3068=CARTESIAN_POINT ( 'NONE',  ( 7.234561953626996335E-06, 0.004097986548672528061, -10.04237554641092345 ) ) ;
#3072=CARTESIAN_POINT ( 'NONE',  ( 7.234561953626996335E-06, 0.004097986548672528061, -10.04237554641092345 ) ) ;
#3074=CARTESIAN_POINT ( 'NONE',  ( -14.09196505061983906, -2.357472998381126672, 29.17523161774379403 ) ) ;
#3077=CARTESIAN_POINT ( 'NONE',  ( -12.37116490068860664, 7.151597986548673624, 17.90262445358908039 ) ) ;
#3079=CARTESIAN_POINT ( 'NONE',  ( 13.86273172203279991, 3.462389489571491730, 30.93651510420201234 ) ) ;
#3083=CIRCLE ( 'NONE', #826, 14.28750000000000142 ) ;
#3084=DIRECTION ( 'NONE',  ( -1.000000000000000000, 0.000000000000000000, 0.000000000000000000 ) ) ;
#3086=ORIENTED_EDGE ( 'NONE', *, *, #3057, .T. ) ;
#3088=AXIS2_PLACEMENT_3D ( 'NONE', #3072, #205, #3381 ) ;
#3090=ORIENTED_EDGE ( 'NONE', *, *, #2618, .F. ) ;
#3101=DIRECTION ( 'NONE',  ( -1.000000000000000000, 0.000000000000000000, 0.000000000000000000 ) ) ;
#3102=VERTEX_POINT ( 'NONE', #1608 ) ;
#3105=ORIENTED_EDGE ( 'NONE', *, *, #3599, .T. ) ;
#3106=DIRECTION ( 'NONE',  ( -0.000000000000000000, -0.000000000000000000, -1.000000000000000000 ) ) ;
#3112=EDGE_CURVE ( 'NONE', #3035, #2613, #793, .T. ) ;
#3114=ADVANCED_FACE ( 'NONE', ( #4094 ), #471, .F. ) ;
#3115=FACE_OUTER_BOUND ( 'NONE', #3421, .T. ) ;
#3122=CARTESIAN_POINT ( 'NONE',  ( -7.619992765438045268, -3.569652013451326322, 31.86762445358909446 ) ) ;
#3130=CARTESIAN_POINT ( 'NONE',  ( 13.60369065225541974, -4.367129746283612945, 37.52732938813279873 ) ) ;
#3131=CARTESIAN_POINT ( 'NONE',  ( 7.234561953626996335E-06, 0.004097986548672528061, -8.542375546410942988 ) ) ;
#3132=ORIENTED_EDGE ( 'NONE', *, *, #996, .F. ) ;
#3133=EDGE_LOOP ( 'NONE', ( #801, #222, #880, #94, #438 ) ) ;
#3135=SURFACE_STYLE_FILL_AREA ( #1711 ) ;
#3136=ORIENTED_EDGE ( 'NONE', *, *, #2321, .T. ) ;
#3143=VECTOR ( 'NONE', #2776, 1000.000000000000000 ) ;
#3147=CARTESIAN_POINT ( 'NONE',  ( -8.369992765438045268, 0.004097986548673428382, 31.86762445358908735 ) ) ;
#3160=SURFACE_STYLE_USAGE ( .BOTH. , #1731 ) ;
#3161=VECTOR ( 'NONE', #88, 1000.000000000000000 ) ;
#3167=CARTESIAN_POINT ( 'NONE',  ( 8.370007234561949616, -6.393402013451325416, 17.90262445358908039 ) ) ;
#3170=FACE_OUTER_BOUND ( 'NONE', #2367, .T. ) ;
#3175=EDGE_CURVE ( 'NONE', #728, #2910, #3962, .T. ) ;
#3176=ADVANCED_FACE ( 'NONE', ( #2544 ), #2808, .T. ) ;
#3177=ORIENTED_EDGE ( 'NONE', *, *, #1103, .T. ) ;
#3178=CARTESIAN_POINT ( 'NONE',  ( 14.10223202603829584, -2.331137260515613097, 38.63906452781715473 ) ) ;
#3181=ORIENTED_EDGE ( 'NONE', *, *, #2584, .T. ) ;
#3184=ORIENTED_EDGE ( 'NONE', *, *, #2983, .T. ) ;
#3187=CARTESIAN_POINT ( 'NONE',  ( -14.12139980767486946, 2.185052774741614190, 29.02700012481545144 ) ) ;
#3192=DIRECTION ( 'NONE',  ( -9.517981353260378315E-33, -8.841607930564763213E-17, 1.000000000000000000 ) ) ;
#3193=DIRECTION ( 'NONE',  ( -1.000000000000000000, 0.000000000000000000, 0.000000000000000000 ) ) ;
#3196=DIRECTION ( 'NONE',  ( 1.000000000000000000, 0.000000000000000000, 0.000000000000000000 ) ) ;
#3202=AXIS2_PLACEMENT_3D ( 'NONE', #4273, #1081, #1055 ) ;
#3208=EDGE_LOOP ( 'NONE', ( #2322, #1361, #167, #1752, #889 ) ) ;
#3212=CIRCLE ( 'NONE', #1195, 0.7499999999999997780 ) ;
#3216=PLANE ( 'NONE',  #2514 ) ;
#3218=DIRECTION ( 'NONE',  ( -1.076498916035107621E-16, -1.000000000000000000, 0.000000000000000000 ) ) ;
#3224=ORIENTED_EDGE ( 'NONE', *, *, #1734, .T. ) ;
#3225=VERTEX_POINT ( 'NONE', #735 ) ;
#3227=CARTESIAN_POINT ( 'NONE',  ( -13.60367618313151361, 4.375325719380958489, 37.52732938813279873 ) ) ;
#3230=CARTESIAN_POINT ( 'NONE',  ( -14.09217321523874489, 2.364479724326565169, 29.17410210810483662 ) ) ;
#3234=DIRECTION ( 'NONE',  ( -1.000000000000000000, 0.000000000000000000, 0.000000000000000000 ) ) ;
#3238=DIRECTION ( 'NONE',  ( 0.000000000000000000, 0.000000000000000000, 1.000000000000000000 ) ) ;
#3239=VECTOR ( 'NONE', #2497, 1000.000000000000000 ) ;
#3240=CARTESIAN_POINT ( 'NONE',  ( 14.28750723456195537, 0.004097986548674313959, 35.44137445358909133 ) ) ;
#3245=ORIENTED_EDGE ( 'NONE', *, *, #995, .T. ) ;
#3248=CARTESIAN_POINT ( 'NONE',  ( -6.869992765438044380, 6.401597986548673624, 17.90262445358908039 ) ) ;
#3249=DIRECTION ( 'NONE',  ( -1.000000000000000000, -1.076498916035107621E-16, 0.000000000000000000 ) ) ;
#3251=EDGE_CURVE ( 'NONE', #1657, #4, #3320, .T. ) ;
#3254=EDGE_LOOP ( 'NONE', ( #1378, #1089, #608, #593 ) ) ;
#3257=CIRCLE ( 'NONE', #3976, 14.28750000000000142 ) ;
#3258=ORIENTED_EDGE ( 'NONE', *, *, #3112, .T. ) ;
#3259=EDGE_CURVE ( 'NONE', #4620, #2910, #4607, .T. ) ;
#3263=CARTESIAN_POINT ( 'NONE',  ( 12.50413115247574503, 6.917199504306219993, 33.74317678317729730 ) ) ;
#3266=CARTESIAN_POINT ( 'NONE',  ( -7.619992765438047044, -6.393402013451324528, 17.15262445358908039 ) ) ;
#3269=CARTESIAN_POINT ( 'NONE',  ( -14.28749276543804925, 0.004097986548672528061, 17.15262445358908039 ) ) ;
#3272=DIRECTION ( 'NONE',  ( 1.000000000000000000, 0.000000000000000000, 0.000000000000000000 ) ) ;
#3274=DIRECTION ( 'NONE',  ( -0.000000000000000000, -0.000000000000000000, -1.000000000000000000 ) ) ;
#3275=EDGE_LOOP ( 'NONE', ( #4548, #1704, #3280, #4278, #684, #2029, #824, #1645 ) ) ;
#3277=( LENGTH_UNIT ( ) NAMED_UNIT ( * ) SI_UNIT ( .MILLI., .METRE. ) );
#3280=ORIENTED_EDGE ( 'NONE', *, *, #3284, .T. ) ;
#3281=CARTESIAN_POINT ( 'NONE',  ( -14.17567385476558606, 1.798747337914841093, 28.76844003329341604 ) ) ;
#3284=EDGE_CURVE ( 'NONE', #338, #4593, #2451, .T. ) ;
#3285=CARTESIAN_POINT ( 'NONE',  ( 2.680752993293609165, -3.565902013451325736, -8.854438399834824835 ) ) ;
#3286=AXIS2_PLACEMENT_3D ( 'NONE', #3131, #2077, #3084 ) ;
#3291=DIRECTION ( 'NONE',  ( 1.000000000000000000, 0.000000000000000000, 0.000000000000000000 ) ) ;
#3294=ORIENTED_EDGE ( 'NONE', *, *, #2821, .T. ) ;
#3301=FACE_OUTER_BOUND ( 'NONE', #3254, .T. ) ;
#3302=ORIENTED_EDGE ( 'NONE', *, *, #286, .T. ) ;
#3303=CIRCLE ( 'NONE', #1879, 0.7500000000000006661 ) ;
#3306=FACE_OUTER_BOUND ( 'NONE', #1399, .T. ) ;
#3308=DIRECTION ( 'NONE',  ( 1.000000000000000000, 0.000000000000000000, 0.000000000000000000 ) ) ;
#3314=ADVANCED_FACE ( 'NONE', ( #3170 ), #2761, .F. ) ;
#3316=CARTESIAN_POINT ( 'NONE',  ( -12.50411668335183002, -6.909003531208875337, 33.74317678317729019 ) ) ;
#3317=B_SPLINE_CURVE_WITH_KNOTS ( 'NONE', 3,
 ( #688, #4365, #3564, #3938, #3961, #733, #34, #1874, #2896, #1480, #3653, #4340, #1127, #2541, #3285, #1155 ),
 .UNSPECIFIED., .F., .F.,
 ( 4, 2, 2, 2, 2, 2, 2, 4 ),
 ( 0.004723219286513068334, 0.006427450678611836346, 0.007279566374661219051, 0.008131682070710601756, 0.008557739918735294410, 0.008983797766759987063, 0.009835913462809368901, 0.01154014485490813431 ),
 .UNSPECIFIED. ) ;
#3320=CIRCLE ( 'NONE', #4524, 0.7500000000000006661 ) ;
#3322=CYLINDRICAL_SURFACE ( 'NONE', #3579, 0.7499999999999997780 ) ;
#3324=VECTOR ( 'NONE', #2740, 1000.000000000000000 ) ;
#3325=CARTESIAN_POINT ( 'NONE',  ( 14.00306357353840880, 2.843936418111722819, 34.04970046675368422 ) ) ;
#3327=ORIENTED_EDGE ( 'NONE', *, *, #3804, .T. ) ;
#3334=CARTESIAN_POINT ( 'NONE',  ( 14.99250723456195544, 7.151597986548670072, 31.86762445358908735 ) ) ;
#3335=CARTESIAN_POINT ( 'NONE',  ( -14.28159961045932214, -0.4665338100600365245, 35.41802149249647158 ) ) ;
#3341=CARTESIAN_POINT ( 'NONE',  ( -13.66280854539549772, -4.179239825960909371, 37.66764907019537389 ) ) ;
#3343=CARTESIAN_POINT ( 'NONE',  ( 14.17609414618484998, -1.787581051912757957, 28.76652967853488008 ) ) ;
#3345=CARTESIAN_POINT ( 'NONE',  ( -17.48249276543803532, -7.143402013451323640, 31.86762445358908735 ) ) ;
#3349=EDGE_CURVE ( 'NONE', #849, #4649, #2330, .T. ) ;
#3352=CARTESIAN_POINT ( 'NONE',  ( 12.27079937262106668, 7.323080895278853752, 17.41529878742303694 ) ) ;
#3354=PLANE ( 'NONE',  #69 ) ;
#3355=CARTESIAN_POINT ( 'NONE',  ( -14.28749276543804569, 0.2413016096126177623, 35.44137445358909133 ) ) ;
#3356=CARTESIAN_POINT ( 'NONE',  ( 7.234561953626996335E-06, 0.004097986548672528061, 17.16762445358907385 ) ) ;
#3362=CARTESIAN_POINT ( 'NONE',  ( 14.28750723456195360, 0.2382004874472088418, 28.29387445358909403 ) ) ;
#3364=VERTEX_POINT ( 'NONE', #2520 ) ;
#3368=CYLINDRICAL_SURFACE ( 'NONE', #3544, 0.7500000000000006661 ) ;
#3371=EDGE_LOOP ( 'NONE', ( #1735, #3979, #1756, #1185 ) ) ;
#3372=CARTESIAN_POINT ( 'NONE',  ( 8.370007234561951392, 0.004097986548671627739, 31.86762445358908735 ) ) ;
#3373=CARTESIAN_POINT ( 'NONE',  ( -12.30670969789281699, -7.253995209643718134, 17.49673779855212885 ) ) ;
#3375=ADVANCED_FACE ( 'NONE', ( #4272 ), #2108, .T. ) ;
#3381=DIRECTION ( 'NONE',  ( -1.000000000000000000, 0.000000000000000000, 0.000000000000000000 ) ) ;
#3383=FACE_OUTER_BOUND ( 'NONE', #4303, .T. ) ;
#3386=EDGE_CURVE ( 'NONE', #1408, #1899, #1067, .T. ) ;
#3387=AXIS2_PLACEMENT_3D ( 'NONE', #461, #2500, #3943 ) ;
#3390=CARTESIAN_POINT ( 'NONE',  ( -3.573742765438046476, 0.004097986548672528061, 17.16762445358907385 ) ) ;
#3395=ADVANCED_FACE ( 'NONE', ( #389 ), #4630, .T. ) ;
#3397=EDGE_CURVE ( 'NONE', #1657, #98, #2474, .T. ) ;
#3406=DIRECTION ( 'NONE',  ( -1.000000000000000000, 1.076498916035107744E-16, 0.000000000000000000 ) ) ;
#3410=STYLED_ITEM ( 'NONE', ( #1382 ), #363 ) ;
#3413=CARTESIAN_POINT ( 'NONE',  ( 14.17558134697462968, 1.799572313586632610, 28.76893179367983677 ) ) ;
#3415=SHAPE_REPRESENTATION ( 'Part 131_Varsay\X2\0131\X0\lan', ( #4483 ), #4021 ) ;
#3420=ORIENTED_EDGE ( 'NONE', *, *, #2659, .T. ) ;
#3421=EDGE_LOOP ( 'NONE', ( #157, #2116, #3445, #3105, #3184 ) ) ;
#3425=ORIENTED_EDGE ( 'NONE', *, *, #1625, .T. ) ;
#3428=EDGE_CURVE ( 'NONE', #4575, #2026, #1080, .T. ) ;
#3429=FACE_OUTER_BOUND ( 'NONE', #3859, .T. ) ;
#3430=CARTESIAN_POINT ( 'NONE',  ( -14.24230335822356430, 1.160144388813159733, 35.25732888177847713 ) ) ;
#3431=CARTESIAN_POINT ( 'NONE',  ( 14.28750723456195537, 0.004097986548674278397, 17.15262445358908039 ) ) ;
#3436=LINE ( 'NONE', #111, #2609 ) ;
#3438=DIRECTION ( 'NONE',  ( -1.076498916035107621E-16, 1.000000000000000000, 0.000000000000000000 ) ) ;
#3445=ORIENTED_EDGE ( 'NONE', *, *, #810, .T. ) ;
#3449=UNCERTAINTY_MEASURE_WITH_UNIT (LENGTH_MEASURE( 1.000000000000000082E-05 ), #2993, 'distance_accuracy_value', 'NONE');
#3451=AXIS2_PLACEMENT_3D ( 'NONE', #3984, #2539, #1457 ) ;
#3452=FACE_OUTER_BOUND ( 'NONE', #794, .T. ) ;
#3457=CARTESIAN_POINT ( 'NONE',  ( 12.37117936981251987, 7.151597986548670072, 31.86762445358908735 ) ) ;
#3459=CARTESIAN_POINT ( 'NONE',  ( -13.83332089671217524, -3.569652013451325878, 31.63186830820603745 ) ) ;
#3461=AXIS2_PLACEMENT_3D ( 'NONE', #63, #1835, #347 ) ;
#3464=CARTESIAN_POINT ( 'NONE',  ( 14.28750723456195537, 0.004097986548674278397, 28.29387445358909403 ) ) ;
#3465=ORIENTED_EDGE ( 'NONE', *, *, #2940, .T. ) ;
#3466=EDGE_CURVE ( 'NONE', #98, #1569, #2559, .T. ) ;
#3470=CARTESIAN_POINT ( 'NONE',  ( 8.370007234561949616, -6.393402013451324528, 3.292624453589076960 ) ) ;
#3471=VERTEX_POINT ( 'NONE', #503 ) ;
#3491=AXIS2_PLACEMENT_3D ( 'NONE', #3623, #3274, #3642 ) ;
#3503=CARTESIAN_POINT ( 'NONE',  ( 11.96600771949147735, -7.803534059577478033, 17.15262445358908039 ) ) ;
#3507=ORIENTED_EDGE ( 'NONE', *, *, #3397, .T. ) ;
#3509=DIRECTION ( 'NONE',  ( 0.000000000000000000, 0.000000000000000000, 1.000000000000000000 ) ) ;
#3510=ORIENTED_EDGE ( 'NONE', *, *, #3789, .F. ) ;
#3512=ADVANCED_FACE ( 'NONE', ( #3306, #2944 ), #831, .T. ) ;
#3513=DIRECTION ( 'NONE',  ( -0.000000000000000000, -0.000000000000000000, -1.000000000000000000 ) ) ;
#3523=CIRCLE ( 'NONE', #3451, 3.573749999999999538 ) ;
#3525=CARTESIAN_POINT ( 'NONE',  ( -14.00273932899718687, -2.837234857420575018, 29.68761152008073267 ) ) ;
#3528=CARTESIAN_POINT ( 'NONE',  ( 11.90639837545767499, -7.893402013451324528, 17.15262445358908039 ) ) ;
#3538=VECTOR ( 'NONE', #155, 1000.000000000000000 ) ;
#3539=ORIENTED_EDGE ( 'NONE', *, *, #20, .F. ) ;
#3542=CARTESIAN_POINT ( 'NONE',  ( -13.87969794115237399, 3.394527399177292626, 30.71358080212464259 ) ) ;
#3543=VECTOR ( 'NONE', #2648, 1000.000000000000000 ) ;
#3544=AXIS2_PLACEMENT_3D ( 'NONE', #901, #4384, #446 ) ;
#3548=DIRECTION ( 'NONE',  ( 0.000000000000000000, 0.000000000000000000, -1.000000000000000000 ) ) ;
#3549=PRODUCT_DEFINITION_SHAPE ( 'NONE', 'NONE',  #3694 ) ;
#3553=ORIENTED_EDGE ( 'NONE', *, *, #404, .F. ) ;
#3554=CARTESIAN_POINT ( 'NONE',  ( 13.42338109688237502, -4.892394157346815931, 37.07949484329716938 ) ) ;
#3564=CARTESIAN_POINT ( 'NONE',  ( -2.181621296273096533, -3.565902013451326180, -9.148124867462044563 ) ) ;
#3565=CARTESIAN_POINT ( 'NONE',  ( 7.234561953626996335E-06, 0.004097986548672528061, 17.15262445358908039 ) ) ;
#3568=DIRECTION ( 'NONE',  ( -1.076498916035107621E-16, 1.000000000000000000, 0.000000000000000000 ) ) ;
#3569=CARTESIAN_POINT ( 'NONE',  ( 3.152229664848242408, -3.565902013451327068, -10.04237554641092345 ) ) ;
#3570=DIRECTION ( 'NONE',  ( -0.000000000000000000, -0.000000000000000000, 1.000000000000000000 ) ) ;
#3574=CARTESIAN_POINT ( 'NONE',  ( 7.620007234561953169, 0.004097986548671708404, 31.86762445358909446 ) ) ;
#3575=AXIS2_PLACEMENT_3D ( 'NONE', #345, #3918, #2854 ) ;
#3579=AXIS2_PLACEMENT_3D ( 'NONE', #3581, #4600, #1362 ) ;
#3581=CARTESIAN_POINT ( 'NONE',  ( 6.870007234561952281, 12.08996809382683857, 17.90262445358908039 ) ) ;
#3582=CARTESIAN_POINT ( 'NONE',  ( 12.37117936981251987, 7.151597986548668295, 17.15262445358908039 ) ) ;
#3588=CARTESIAN_POINT ( 'NONE',  ( 7.234561953626996335E-06, 0.004097986548672528061, -10.04237554641092345 ) ) ;
#3594=DIRECTION ( 'NONE',  ( 0.000000000000000000, 0.000000000000000000, 1.000000000000000000 ) ) ;
#3596=ORIENTED_EDGE ( 'NONE', *, *, #1849, .T. ) ;
#3597=CARTESIAN_POINT ( 'NONE',  ( -8.369992765438045268, -7.893402013451322752, 17.90262445358908039 ) ) ;
#3598=CARTESIAN_POINT ( 'NONE',  ( -14.16477841556124062, -1.878420794868401300, 38.76682706999738315 ) ) ;
#3599=EDGE_CURVE ( 'NONE', #3603, #116, #4577, .T. ) ;
#3603=VERTEX_POINT ( 'NONE', #637 ) ;
#3604=AXIS2_PLACEMENT_3D ( 'NONE', #369, #2247, #3291 ) ;
#3605=CARTESIAN_POINT ( 'NONE',  ( -12.76993684346950708, 6.415192739153763313, 35.06135232679011438 ) ) ;
#3606=ORIENTED_EDGE ( 'NONE', *, *, #3734, .F. ) ;
#3607=ORIENTED_EDGE ( 'NONE', *, *, #3929, .F. ) ;
#3610=CARTESIAN_POINT ( 'NONE',  ( 12.87896255196901407, 6.196505624857743477, 35.46704985752300843 ) ) ;
#3616=AXIS2_PLACEMENT_3D ( 'NONE', #1030, #936, #4201 ) ;
#3617=DIRECTION ( 'NONE',  ( -1.000000000000000000, 1.076498916035107621E-16, 0.000000000000000000 ) ) ;
#3622=CARTESIAN_POINT ( 'NONE',  ( -13.11702252608348651, -5.661701175589295865, 36.23092228855526997 ) ) ;
#3623=CARTESIAN_POINT ( 'NONE',  ( 7.234561953626996335E-06, 0.004097986548672528061, 3.292624453589077405 ) ) ;
#3627=MECHANICAL_DESIGN_GEOMETRIC_PRESENTATION_REPRESENTATION('',(#3410),#621);
#3630=CARTESIAN_POINT ( 'NONE',  ( -13.94802501356800661, 3.102887394450430047, 30.07232133647258010 ) ) ;
#3632=CARTESIAN_POINT ( 'NONE',  ( 14.28750723456195537, 0.004097986548674278397, 39.01512445358908820 ) ) ;
#3637=CARTESIAN_POINT ( 'NONE',  ( -14.24206744302798633, -1.154622011196222653, 35.25632758055221672 ) ) ;
#3638=CARTESIAN_POINT ( 'NONE',  ( -8.369992765438045268, 0.004097986548673428382, 31.86762445358908735 ) ) ;
#3642=DIRECTION ( 'NONE',  ( 1.000000000000000000, 0.000000000000000000, 0.000000000000000000 ) ) ;
#3644=SHAPE_DEFINITION_REPRESENTATION ( #3549, #3415 ) ;
#3646=CARTESIAN_POINT ( 'NONE',  ( -12.47853676740481887, 6.962653799640055929, 33.51726641232498594 ) ) ;
#3650=DIRECTION ( 'NONE',  ( 1.000000000000000000, 0.000000000000000000, -0.000000000000000000 ) ) ;
#3653=CARTESIAN_POINT ( 'NONE',  ( 0.7146566484001382058, -3.565902013451327957, -9.666548897786826799 ) ) ;
#3654=AXIS2_PLACEMENT_3D ( 'NONE', #3638, #371, #4015 ) ;
#3657=LINE ( 'NONE', #3266, #717 ) ;
#3658=EDGE_CURVE ( 'NONE', #4593, #2966, #954, .T. ) ;
#3660=CARTESIAN_POINT ( 'NONE',  ( 14.00317140236440849, -2.835233378172992591, 34.05045963228912598 ) ) ;
#3662=AXIS2_PLACEMENT_3D ( 'NONE', #3597, #2183, #2579 ) ;
#3663=ORIENTED_EDGE ( 'NONE', *, *, #3599, .F. ) ;
#3666=VECTOR ( 'NONE', #78, 1000.000000000000000 ) ;
#3672=CIRCLE ( 'NONE', #372, 3.573749999999999538 ) ;
#3675=CARTESIAN_POINT ( 'NONE',  ( -11.96610561084410840, -7.803364663213757879, 17.15262445358908039 ) ) ;
#3678=VERTEX_POINT ( 'NONE', #1651 ) ;
#3681=CYLINDRICAL_SURFACE ( 'NONE', #3387, 7.147499999999999076 ) ;
#3682=CIRCLE ( 'NONE', #1061, 1.499999999999999556 ) ;
#3686=DIRECTION ( 'NONE',  ( 0.000000000000000000, 0.000000000000000000, -1.000000000000000000 ) ) ;
#3691=CARTESIAN_POINT ( 'NONE',  ( 14.20095123608300014, -1.580981516206518833, 28.65617994343129382 ) ) ;
#3693=LINE ( 'NONE', #2281, #2768 ) ;
#3694=PRODUCT_DEFINITION ( 'UNKNOWN', '', #416, #2677 ) ;
#3696=DIRECTION ( 'NONE',  ( 1.000000000000000000, -1.076498916035107621E-16, -0.000000000000000000 ) ) ;
#3699=DIRECTION ( 'NONE',  ( 0.000000000000000000, 0.000000000000000000, 1.000000000000000000 ) ) ;
#3700=ADVANCED_FACE ( 'NONE', ( #4531 ), #2615, .T. ) ;
#3702=ORIENTED_EDGE ( 'NONE', *, *, #4276, .T. ) ;
#3703=DIRECTION ( 'NONE',  ( 0.000000000000000000, 0.000000000000000000, 1.000000000000000000 ) ) ;
#3704=DIRECTION ( 'NONE',  ( 1.000000000000000000, 0.000000000000000000, 0.000000000000000000 ) ) ;
#3708=AXIS2_PLACEMENT_3D ( 'NONE', #2653, #442, #1909 ) ;
#3710=EDGE_LOOP ( 'NONE', ( #2909, #472, #4169, #705 ) ) ;
#3715=CYLINDRICAL_SURFACE ( 'NONE', #4409, 0.7499999999999997780 ) ;
#3718=EDGE_LOOP ( 'NONE', ( #2563, #1605, #4185, #1293, #4424, #751 ) ) ;
#3723=ORIENTED_EDGE ( 'NONE', *, *, #260, .F. ) ;
#3725=ADVANCED_FACE ( 'NONE', ( #3452 ), #1321, .T. ) ;
#3726=CARTESIAN_POINT ( 'NONE',  ( 8.370007234561949616, 6.401597986548672736, 31.86762445358908735 ) ) ;
#3728=DIRECTION ( 'NONE',  ( 1.000000000000000000, 0.000000000000000000, -0.000000000000000000 ) ) ;
#3730=ORIENTED_EDGE ( 'NONE', *, *, #870, .T. ) ;
#3732=CIRCLE ( 'NONE', #3286, 4.762499999999999289 ) ;
#3733=CARTESIAN_POINT ( 'NONE',  ( 14.24248549217296400, 1.158197531232292299, 28.47721150812772350 ) ) ;
#3734=EDGE_CURVE ( 'NONE', #254, #3850, #3523, .T. ) ;
#3736=ADVANCED_FACE ( 'NONE', ( #2170 ), #757, .T. ) ;
#3738=CARTESIAN_POINT ( 'NONE',  ( 14.09194898772133975, -2.357612872106044311, 29.17542961446211081 ) ) ;
#3743=CARTESIAN_POINT ( 'NONE',  ( 14.28750723456195715, 0.2398388336121953790, 35.44137445358909133 ) ) ;
#3749=EDGE_LOOP ( 'NONE', ( #1557, #3932 ) ) ;
#3752=CARTESIAN_POINT ( 'NONE',  ( 0.000000000000000000, 0.000000000000000000, 0.000000000000000000 ) ) ;
#3753=LINE ( 'NONE', #2665, #292 ) ;
#3754=CARTESIAN_POINT ( 'NONE',  ( -14.28159378806564206, 0.4743560429282985824, 35.41799410330143161 ) ) ;
#3758=LINE ( 'NONE', #3077, #1653 ) ;
#3764=EDGE_CURVE ( 'NONE', #4454, #1093, #1762, .T. ) ;
#3768=CARTESIAN_POINT ( 'NONE',  ( 14.17575381291738523, 1.798219341900524348, 34.96710348429465398 ) ) ;
#3769=EDGE_CURVE ( 'NONE', #1498, #1942, #665, .T. ) ;
#3781=ORIENTED_EDGE ( 'NONE', *, *, #3349, .F. ) ;
#3782=CARTESIAN_POINT ( 'NONE',  ( 18.74250723456195189, 0.004097986548670510577, 31.86762445358909446 ) ) ;
#3785=CARTESIAN_POINT ( 'NONE',  ( 14.12134054576453934, 2.185513808779087963, 29.02736931185435054 ) ) ;
#3787=ORIENTED_EDGE ( 'NONE', *, *, #2659, .F. ) ;
#3789=EDGE_CURVE ( 'NONE', #4140, #849, #4532, .T. ) ;
#3794=ORIENTED_EDGE ( 'NONE', *, *, #1220, .F. ) ;
#3804=EDGE_CURVE ( 'NONE', #1869, #1569, #2145, .T. ) ;
#3805=CARTESIAN_POINT ( 'NONE',  ( 11.90639837545767499, -7.893402013451324528, 17.15262445358908039 ) ) ;
#3816=CARTESIAN_POINT ( 'NONE',  ( -7.619992765438045268, 0.004097986548673348585, 31.86762445358909446 ) ) ;
#3817=ORIENTED_EDGE ( 'NONE', *, *, #2751, .F. ) ;
#3822=DIRECTION ( 'NONE',  ( 0.000000000000000000, 0.000000000000000000, 1.000000000000000000 ) ) ;
#3827=ORIENTED_EDGE ( 'NONE', *, *, #2174, .F. ) ;
#3830=CARTESIAN_POINT ( 'NONE',  ( 12.58716276799420797, -6.756261061128872036, 34.20002532364929237 ) ) ;
#3831=CARTESIAN_POINT ( 'NONE',  ( -12.37116490068861197, -7.143402013451321864, 17.15262445358908039 ) ) ;
#3834=ORIENTED_EDGE ( 'NONE', *, *, #734, .F. ) ;
#3838=AXIS2_PLACEMENT_3D ( 'NONE', #3356, #2997, #4465 ) ;
#3849=VECTOR ( 'NONE', #3513, 1000.000000000000000 ) ;
#3850=VERTEX_POINT ( 'NONE', #4142 ) ;
#3852=FACE_OUTER_BOUND ( 'NONE', #405, .T. ) ;
#3854=ADVANCED_FACE ( 'NONE', ( #1261, #564 ), #897, .F. ) ;
#3859=EDGE_LOOP ( 'NONE', ( #3730, #91, #277, #1967, #2674 ) ) ;
#3867=CARTESIAN_POINT ( 'NONE',  ( -14.03274124047852744, -2.687123044775775238, 29.50471817954215581 ) ) ;
#3868=DIRECTION ( 'NONE',  ( -0.000000000000000000, -0.000000000000000000, -1.000000000000000000 ) ) ;
#3873=CARTESIAN_POINT ( 'NONE',  ( 8.370007234561949616, 6.401597986548672736, 17.90262445358908039 ) ) ;
#3875=AXIS2_PLACEMENT_3D ( 'NONE', #4218, #636, #4240 ) ;
#3877=EDGE_CURVE ( 'NONE', #3060, #3850, #3056, .T. ) ;
#3879=DIRECTION ( 'NONE',  ( 9.517981353260378315E-33, -8.841607930564763213E-17, 1.000000000000000000 ) ) ;
#3880=AXIS2_PLACEMENT_3D ( 'NONE', #2434, #587, #2009 ) ;
#3886=DIRECTION ( 'NONE',  ( 0.000000000000000000, 0.000000000000000000, 1.000000000000000000 ) ) ;
#3896=CARTESIAN_POINT ( 'NONE',  ( 7.620007234561951392, 12.08996809382683857, 17.90262445358908039 ) ) ;
#3898=AXIS2_PLACEMENT_3D ( 'NONE', #3726, #4085, #1298 ) ;
#3901=FACE_OUTER_BOUND ( 'NONE', #903, .T. ) ;
#3904=EDGE_LOOP ( 'NONE', ( #3038, #3420, #4432, #3136 ) ) ;
#3905=AXIS2_PLACEMENT_3D ( 'NONE', #4555, #4221, #1001 ) ;
#3907=VERTEX_POINT ( 'NONE', #654 ) ;
#3909=CARTESIAN_POINT ( 'NONE',  ( -14.28749276543805102, 0.2378296109429726690, 28.29387445358910469 ) ) ;
#3918=DIRECTION ( 'NONE',  ( -0.000000000000000000, -0.000000000000000000, -1.000000000000000000 ) ) ;
#3920=DIRECTION ( 'NONE',  ( -0.000000000000000000, -0.000000000000000000, -1.000000000000000000 ) ) ;
#3921=TOROIDAL_SURFACE ( 'NONE', #1074, 6.397499999999999964, 0.7500000000000000000 ) ;
#3922=ORIENTED_EDGE ( 'NONE', *, *, #3175, .F. ) ;
#3927=B_SPLINE_CURVE_WITH_KNOTS ( 'NONE', 3,
 ( #4079, #3675, #148, #1919, #102, #4124, #3373, #453, #1945, #2616 ),
 .UNSPECIFIED., .F., .F.,
 ( 4, 2, 2, 2, 4 ),
 ( 0.000000000000000000, 0.0003186827706029869483, 0.0006373655412059738967, 0.0009560483118089608450, 0.001274731082411947793 ),
 .UNSPECIFIED. ) ;
#3928=ORIENTED_EDGE ( 'NONE', *, *, #3175, .T. ) ;
#3929=EDGE_CURVE ( 'NONE', #2486, #2613, #3968, .T. ) ;
#3930=CARTESIAN_POINT ( 'NONE',  ( -13.05553636216897573, 5.809745059568978576, 36.04312068514321510 ) ) ;
#3932=ORIENTED_EDGE ( 'NONE', *, *, #2676, .F. ) ;
#3938=CARTESIAN_POINT ( 'NONE',  ( -1.395705466780353232, -3.565902013451327512, -9.479113238741371461 ) ) ;
#3940=EDGE_CURVE ( 'NONE', #1513, #4636, #1401, .T. ) ;
#3942=CARTESIAN_POINT ( 'NONE',  ( -8.369992765438045268, -6.393402013451324528, 17.90262445358908039 ) ) ;
#3943=DIRECTION ( 'NONE',  ( 0.000000000000000000, -1.000000000000000000, 0.000000000000000000 ) ) ;
#3948=CARTESIAN_POINT ( 'NONE',  ( -13.48443111421813256, -4.722189432810507626, 37.23438744284855773 ) ) ;
#3950=VECTOR ( 'NONE', #3868, 1000.000000000000000 ) ;
#3957=DIRECTION ( 'NONE',  ( -0.000000000000000000, -0.000000000000000000, -1.000000000000000000 ) ) ;
#3961=CARTESIAN_POINT ( 'NONE',  ( -1.123311860454918376, -3.565902013451327068, -9.572186130557330586 ) ) ;
#3962=LINE ( 'NONE', #1768, #1767 ) ;
#3965=VECTOR ( 'NONE', #4226, 1000.000000000000000 ) ;
#3967=CARTESIAN_POINT ( 'NONE',  ( 14.17614002078996727, -1.787162261592786683, 34.96891191078774597 ) ) ;
#3968=CIRCLE ( 'NONE', #216, 4.762499999999999289 ) ;
#3971=ORIENTED_EDGE ( 'NONE', *, *, #263, .T. ) ;
#3975=ORIENTED_EDGE ( 'NONE', *, *, #846, .F. ) ;
#3976=AXIS2_PLACEMENT_3D ( 'NONE', #4170, #1121, #1092 ) ;
#3978=B_SPLINE_CURVE_WITH_KNOTS ( 'NONE', 3,
 ( #1913, #4070, #1443, #3263, #709, #58, #3610, #1460, #2173, #1502, #2570, #1100, #340, #2148, #1829, #1049, #2850, #4010, #780, #759, #4294, #2517, #2198, #3632 ),
 .UNSPECIFIED., .F., .F.,
 ( 4, 2, 2, 2, 2, 2, 2, 2, 2, 2, 2, 4 ),
 ( 0.000000000000000000, 0.001420218485702549145, 0.002840436971405098290, 0.004260655457107647218, 0.004970764699958913659, 0.005680873942810180099, 0.006390983185661445673, 0.007101092428512711247, 0.008521310914215231985, 0.009231420157066490620, 0.009941529399917750989, 0.01136174788562027173 ),
 .UNSPECIFIED. ) ;
#3979=ORIENTED_EDGE ( 'NONE', *, *, #4196, .T. ) ;
#3984=CARTESIAN_POINT ( 'NONE',  ( 7.234561953626996335E-06, 0.004097986548672528061, 17.15262445358908039 ) ) ;
#3988=CARTESIAN_POINT ( 'NONE',  ( 6.870007234561953169, 0.004097986548673267920, 17.15262445358908039 ) ) ;
#3991=CARTESIAN_POINT ( 'NONE',  ( 14.28750723456195537, 0.004097986548674278397, 39.01512445358908820 ) ) ;
#3992=VECTOR ( 'NONE', #1463, 1000.000000000000000 ) ;
#3997=CARTESIAN_POINT ( 'NONE',  ( -13.30104646604472407, -5.215534672250015547, 36.75583910459432957 ) ) ;
#4002=( NAMED_UNIT ( * ) SI_UNIT ( $, .STERADIAN. ) SOLID_ANGLE_UNIT ( ) );
#4003=ADVANCED_FACE ( 'NONE', ( #3852 ), #4571, .F. ) ;
#4010=CARTESIAN_POINT ( 'NONE',  ( 14.05881308173377775, 2.559578388020689488, 38.54673083970038761 ) ) ;
#4012=CARTESIAN_POINT ( 'NONE',  ( 7.620007234561954057, -6.393402013451328081, 31.86762445358908735 ) ) ;
#4014=CARTESIAN_POINT ( 'NONE',  ( -14.17582073965153278, -1.789560200172800153, 34.96752390565762880 ) ) ;
#4015=DIRECTION ( 'NONE',  ( 0.000000000000000000, -1.000000000000000000, 0.000000000000000000 ) ) ;
#4018=DIRECTION ( 'NONE',  ( 0.000000000000000000, 1.000000000000000000, -0.000000000000000000 ) ) ;
#4019=ORIENTED_EDGE ( 'NONE', *, *, #114, .F. ) ;
#4021=( GEOMETRIC_REPRESENTATION_CONTEXT ( 3 ) GLOBAL_UNCERTAINTY_ASSIGNED_CONTEXT ( ( #3449 ) ) GLOBAL_UNIT_ASSIGNED_CONTEXT ( ( #2993, #4438, #1574 ) ) REPRESENTATION_CONTEXT ( 'NONE', 'WORKASPACE' ) );
#4030=DIRECTION ( 'NONE',  ( 0.000000000000000000, 0.000000000000000000, -1.000000000000000000 ) ) ;
#4034=AXIS2_PLACEMENT_3D ( 'NONE', #3816, #4150, #4507 ) ;
#4037=CARTESIAN_POINT ( 'NONE',  ( -13.83332089671217346, -3.569652013451324990, 32.10328778829815377 ) ) ;
#4050=CIRCLE ( 'NONE', #3898, 0.7500000000000006661 ) ;
#4053=CARTESIAN_POINT ( 'NONE',  ( 18.74250723456195189, -3.569652013451328987, 31.86762445358909446 ) ) ;
#4058=CARTESIAN_POINT ( 'NONE',  ( 3.573757234561953045, 0.004097986548672966078, 17.16762445358907385 ) ) ;
#4059=CARTESIAN_POINT ( 'NONE',  ( -13.83332089671217169, 3.577847986548673642, 31.86762445358909446 ) ) ;
#4060=DIRECTION ( 'NONE',  ( 1.000000000000000000, 0.000000000000000000, 0.000000000000000000 ) ) ;
#4065=DIRECTION ( 'NONE',  ( -9.517981353260378315E-33, 8.841607930564763213E-17, -1.000000000000000000 ) ) ;
#4069=VECTOR ( 'NONE', #827, 1000.000000000000000 ) ;
#4070=CARTESIAN_POINT ( 'NONE',  ( 12.37117936981251809, 7.151597986548668295, 32.34863974131316411 ) ) ;
#4072=AXIS2_PLACEMENT_3D ( 'NONE', #4447, #2293, #4113 ) ;
#4073=DIRECTION ( 'NONE',  ( -1.355782318074878530E-16, 1.000000000000000000, 0.000000000000000000 ) ) ;
#4076=ORIENTED_EDGE ( 'NONE', *, *, #2471, .F. ) ;
#4079=CARTESIAN_POINT ( 'NONE',  ( -11.90638390633376709, -7.893402013451320975, 17.15262445358908039 ) ) ;
#4082=EDGE_CURVE ( 'NONE', #657, #728, #431, .T. ) ;
#4085=DIRECTION ( 'NONE',  ( 0.000000000000000000, -0.000000000000000000, 1.000000000000000000 ) ) ;
#4086=DIRECTION ( 'NONE',  ( 0.000000000000000000, 0.000000000000000000, -1.000000000000000000 ) ) ;
#4087=DIRECTION ( 'NONE',  ( 0.000000000000000000, 0.000000000000000000, 1.000000000000000000 ) ) ;
#4093=CARTESIAN_POINT ( 'NONE',  ( 14.20066920646721620, 1.591968333033273231, 28.65740429563327396 ) ) ;
#4094=FACE_OUTER_BOUND ( 'NONE', #3710, .T. ) ;
#4099=ORIENTED_EDGE ( 'NONE', *, *, #4428, .T. ) ;
#4101=FACE_OUTER_BOUND ( 'NONE', #1384, .T. ) ;
#4105=AXIS2_PLACEMENT_3D ( 'NONE', #3372, #2964, #878 ) ;
#4113=DIRECTION ( 'NONE',  ( 0.000000000000000000, -1.000000000000000000, 0.000000000000000000 ) ) ;
#4116=EDGE_LOOP ( 'NONE', ( #3723, #1884 ) ) ;
#4122=ORIENTED_EDGE ( 'NONE', *, *, #4567, .T. ) ;
#4124=CARTESIAN_POINT ( 'NONE',  ( -12.27078490349716056, -7.314884922181505544, 17.41529878742304049 ) ) ;
#4126=EDGE_LOOP ( 'NONE', ( #3327, #1896, #3010, #4349 ) ) ;
#4131=FACE_OUTER_BOUND ( 'NONE', #1972, .T. ) ;
#4135=CARTESIAN_POINT ( 'NONE',  ( 12.30738871829480807, -7.252862566945415423, 17.49889617799752983 ) ) ;
#4139=AXIS2_PLACEMENT_3D ( 'NONE', #2996, #4086, #1996 ) ;
#4140=VERTEX_POINT ( 'NONE', #745 ) ;
#4142=CARTESIAN_POINT ( 'NONE',  ( -3.573742765438046476, 0.004097986548672528061, 17.15262445358908039 ) ) ;
#4145=DIRECTION ( 'NONE',  ( 0.000000000000000000, -1.000000000000000000, 0.000000000000000000 ) ) ;
#4150=DIRECTION ( 'NONE',  ( 1.000000000000000000, -1.076498916035107621E-16, -0.000000000000000000 ) ) ;
#4151=UNCERTAINTY_MEASURE_WITH_UNIT (LENGTH_MEASURE( 1.000000000000000082E-05 ), #3277, 'distance_accuracy_value', 'NONE');
#4152=ADVANCED_FACE ( 'NONE', ( #1631 ), #917, .F. ) ;
#4153=ORIENTED_EDGE ( 'NONE', *, *, #2954, .T. ) ;
#4154=DIRECTION ( 'NONE',  ( 1.000000000000000000, 0.000000000000000000, 0.000000000000000000 ) ) ;
#4156=DIRECTION ( 'NONE',  ( 0.000000000000000000, -1.000000000000000000, 0.000000000000000000 ) ) ;
#4160=CARTESIAN_POINT ( 'NONE',  ( -13.86261300049099709, -3.454607104308479393, 30.93839646180238745 ) ) ;
#4165=EDGE_LOOP ( 'NONE', ( #1520, #3258, #3086, #2963 ) ) ;
#4169=ORIENTED_EDGE ( 'NONE', *, *, #251, .F. ) ;
#4170=CARTESIAN_POINT ( 'NONE',  ( 7.234561953626996335E-06, 0.004097986548672528061, 3.292624453589077405 ) ) ;
#4172=CARTESIAN_POINT ( 'NONE',  ( 18.74250723456195189, -3.569652013451328987, 31.86762445358909446 ) ) ;
#4185=ORIENTED_EDGE ( 'NONE', *, *, #404, .T. ) ;
#4186=AXIS2_PLACEMENT_3D ( 'NONE', #4492, #4418, #1206 ) ;
#4187=CARTESIAN_POINT ( 'NONE',  ( 12.87888252809135459, -6.188448225968623539, 35.46669787887593372 ) ) ;
#4188=EDGE_CURVE ( 'NONE', #2437, #2372, #3758, .T. ) ;
#4194=ORIENTED_EDGE ( 'NONE', *, *, #2821, .F. ) ;
#4196=EDGE_CURVE ( 'NONE', #1630, #254, #559, .T. ) ;
#4199=CARTESIAN_POINT ( 'NONE',  ( -14.28749276543804925, 0.004097986548672528061, 39.01512445358908820 ) ) ;
#4201=DIRECTION ( 'NONE',  ( -1.000000000000000000, 0.000000000000000000, -0.000000000000000000 ) ) ;
#4205=CARTESIAN_POINT ( 'NONE',  ( 7.234561953626996335E-06, 0.004097986548672528061, 17.16762445358907385 ) ) ;
#4208=VERTEX_POINT ( 'NONE', #1558 ) ;
#4209=CARTESIAN_POINT ( 'NONE',  ( 13.48425643984108468, -4.722725237461219194, 37.23391125615015795 ) ) ;
#4211=ORIENTED_EDGE ( 'NONE', *, *, #105, .T. ) ;
#4216=EDGE_CURVE ( 'NONE', #1569, #4, #3436, .T. ) ;
#4218=CARTESIAN_POINT ( 'NONE',  ( 7.234561953626996335E-06, 0.004097986548672528061, -10.04237554641092345 ) ) ;
#4221=DIRECTION ( 'NONE',  ( -0.000000000000000000, -0.000000000000000000, 1.000000000000000000 ) ) ;
#4223=ADVANCED_FACE ( 'NONE', ( #3383 ), #2627, .T. ) ;
#4224=CARTESIAN_POINT ( 'NONE',  ( -14.20090685550316323, -1.581291399450686752, 28.65630886300585800 ) ) ;
#4226=DIRECTION ( 'NONE',  ( 9.517981353260378315E-33, -8.841607930564763213E-17, 1.000000000000000000 ) ) ;
#4228=DIRECTION ( 'NONE',  ( 0.000000000000000000, 0.000000000000000000, -1.000000000000000000 ) ) ;
#4235=CYLINDRICAL_SURFACE ( 'NONE', #101, 0.7499999999999997780 ) ;
#4240=DIRECTION ( 'NONE',  ( 1.000000000000000000, 0.000000000000000000, 0.000000000000000000 ) ) ;
#4242=CARTESIAN_POINT ( 'NONE',  ( -7.619992765438044380, 12.08996809382683857, 17.90262445358908039 ) ) ;
#4244=CARTESIAN_POINT ( 'NONE',  ( -11.90638390633376531, 7.901597986548672736, 17.15262445358908039 ) ) ;
#4249=DIRECTION ( 'NONE',  ( -1.000000000000000000, -0.000000000000000000, -0.000000000000000000 ) ) ;
#4253=CARTESIAN_POINT ( 'NONE',  ( -7.619992765438044380, 6.401597986548673624, 31.86762445358908735 ) ) ;
#4256=CARTESIAN_POINT ( 'NONE',  ( 12.47855123652872322, -6.954457826542711274, 33.51726641232498594 ) ) ;
#4257=CIRCLE ( 'NONE', #1414, 1.499999999999999556 ) ;
#4260=VECTOR ( 'NONE', #3696, 1000.000000000000000 ) ;
#4270=CARTESIAN_POINT ( 'NONE',  ( 8.370007234561949616, 6.401597986548672736, 17.90262445358908039 ) ) ;
#4272=FACE_OUTER_BOUND ( 'NONE', #4471, .T. ) ;
#4273=CARTESIAN_POINT ( 'NONE',  ( 7.234561953626996335E-06, 0.004097986548672528061, -1.469875546410923661 ) ) ;
#4274=CARTESIAN_POINT ( 'NONE',  ( -3.262492765438076869, 0.004097986548673020722, -10.04237554641092345 ) ) ;
#4276=EDGE_CURVE ( 'NONE', #2052, #696, #4306, .T. ) ;
#4277=CIRCLE ( 'NONE', #2463, 0.7500000000000006661 ) ;
#4278=ORIENTED_EDGE ( 'NONE', *, *, #4608, .T. ) ;
#4279=CARTESIAN_POINT ( 'NONE',  ( 12.51138117596144994, -6.895500623138680396, 33.74860486214564048 ) ) ;
#4282=ORIENTED_EDGE ( 'NONE', *, *, #2893, .T. ) ;
#4283=ORIENTED_EDGE ( 'NONE', *, *, #4345, .F. ) ;
#4285=AXIS2_PLACEMENT_3D ( 'NONE', #3167, #4605, #2085 ) ;
#4287=DIRECTION ( 'NONE',  ( 1.000000000000000000, 0.000000000000000000, 0.000000000000000000 ) ) ;
#4290=EDGE_CURVE ( 'NONE', #971, #4494, #2787, .T. ) ;
#4294=CARTESIAN_POINT ( 'NONE',  ( 14.19373809557357191, 1.654917666244543284, 38.82591248395576855 ) ) ;
#4303=EDGE_LOOP ( 'NONE', ( #2929, #3922, #1823, #2237 ) ) ;
#4305=CARTESIAN_POINT ( 'NONE',  ( -12.37116490068861374, -7.143402013451327193, 32.34863974131315700 ) ) ;
#4306=B_SPLINE_CURVE_WITH_KNOTS ( 'NONE', 3,
 ( #864, #539, #1979, #4135, #4495, #2002, #1278, #1746, #3503, #3805 ),
 .UNSPECIFIED., .F., .F.,
 ( 4, 2, 2, 2, 4 ),
 ( 0.000000000000000000, 0.0003199342119934982936, 0.0006398684239869965873, 0.0009598026359804948809, 0.001279736847973993175 ),
 .UNSPECIFIED. ) ;
#4307=DIRECTION ( 'NONE',  ( 0.000000000000000000, -1.000000000000000000, 0.000000000000000000 ) ) ;
#4308=EDGE_LOOP ( 'NONE', ( #2405, #3971, #1334, #2990 ) ) ;
#4310=CARTESIAN_POINT ( 'NONE',  ( -13.30083662496763530, 5.224265971132247444, 36.75526953962744869 ) ) ;
#4314=ORIENTED_EDGE ( 'NONE', *, *, #2041, .T. ) ;
#4315=CARTESIAN_POINT ( 'NONE',  ( -14.00292651309607095, 2.844510957948676033, 29.68641762507535020 ) ) ;
#4321=CARTESIAN_POINT ( 'NONE',  ( -14.28749276543804925, 0.004097986548672528061, 3.292624453589077405 ) ) ;
#4323=CARTESIAN_POINT ( 'NONE',  ( 13.92261338244811952, -3.205599502867460870, 33.45626019218369862 ) ) ;
#4329=DIRECTION ( 'NONE',  ( -2.312964634635740689E-15, 0.000000000000000000, -1.000000000000000000 ) ) ;
#4338=CARTESIAN_POINT ( 'NONE',  ( -14.24246428466184078, 1.158051217861460591, 28.47725504917529804 ) ) ;
#4340=CARTESIAN_POINT ( 'NONE',  ( 1.130815084004146875, -3.565902013451327068, -9.569796636679910762 ) ) ;
#4345=EDGE_CURVE ( 'NONE', #2227, #2910, #2220, .T. ) ;
#4349=ORIENTED_EDGE ( 'NONE', *, *, #870, .F. ) ;
#4353=VECTOR ( 'NONE', #2759, 1000.000000000000000 ) ;
#4359=CARTESIAN_POINT ( 'NONE',  ( -13.93189333643315564, 3.202255926420866761, 38.27679835742612369 ) ) ;
#4362=AXIS2_PLACEMENT_3D ( 'NONE', #1772, #2133, #3196 ) ;
#4365=CARTESIAN_POINT ( 'NONE',  ( -2.677025490679457498, -3.565902013451327068, -8.856895997200147974 ) ) ;
#4374=LINE ( 'NONE', #1161, #164 ) ;
#4376=CARTESIAN_POINT ( 'NONE',  ( 14.28750723456195715, -0.2301263156859972014, 28.29387445358909758 ) ) ;
#4379=CARTESIAN_POINT ( 'NONE',  ( -12.58213841360289820, -6.768164877760692200, 34.20015322194398522 ) ) ;
#4384=DIRECTION ( 'NONE',  ( 1.000000000000000000, -1.076498916035107744E-16, 0.000000000000000000 ) ) ;
#4386=ORIENTED_EDGE ( 'NONE', *, *, #3658, .T. ) ;
#4389=CIRCLE ( 'NONE', #3491, 4.762499999999999289 ) ;
#4390=LINE ( 'NONE', #4410, #4069 ) ;
#4391=ORIENTED_EDGE ( 'NONE', *, *, #4188, .T. ) ;
#4393=CARTESIAN_POINT ( 'NONE',  ( -13.83332089671217169, -3.569652013451326322, 31.86762445358909446 ) ) ;
#4395=CARTESIAN_POINT ( 'NONE',  ( -14.25898534185092004, -0.9269869019229697304, 35.32593247230593647 ) ) ;
#4399=CARTESIAN_POINT ( 'NONE',  ( -14.28749276543804037, -0.4768660484013518830, 39.01512445358906689 ) ) ;
#4407=ORIENTED_EDGE ( 'NONE', *, *, #871, .T. ) ;
#4409=AXIS2_PLACEMENT_3D ( 'NONE', #1937, #95, #1542 ) ;
#4410=CARTESIAN_POINT ( 'NONE',  ( 8.370007234561949616, -7.893402013451324528, 17.15262445358908039 ) ) ;
#4411=ORIENTED_EDGE ( 'NONE', *, *, #3386, .F. ) ;
#4412=AXIS2_PLACEMENT_3D ( 'NONE', #509, #2973, #1953 ) ;
#4416=CARTESIAN_POINT ( 'NONE',  ( -13.87980694821278149, -3.385868028865885115, 33.02271771428084435 ) ) ;
#4418=DIRECTION ( 'NONE',  ( -0.000000000000000000, -0.000000000000000000, -1.000000000000000000 ) ) ;
#4419=AXIS2_PLACEMENT_3D ( 'NONE', #2699, #2275, #2338 ) ;
#4422=DIRECTION ( 'NONE',  ( 1.000000000000000000, -1.076498916035107621E-16, 0.000000000000000000 ) ) ;
#4424=ORIENTED_EDGE ( 'NONE', *, *, #105, .F. ) ;
#4425=CARTESIAN_POINT ( 'NONE',  ( 14.00292109500077231, -2.836439352166247208, 29.68646118753943952 ) ) ;
#4428=EDGE_CURVE ( 'NONE', #1513, #1644, #2810, .T. ) ;
#4432=ORIENTED_EDGE ( 'NONE', *, *, #1103, .F. ) ;
#4438=( NAMED_UNIT ( * ) PLANE_ANGLE_UNIT ( ) SI_UNIT ( $, .RADIAN. ) );
#4439=DIRECTION ( 'NONE',  ( 0.000000000000000000, -1.000000000000000000, 0.000000000000000000 ) ) ;
#4443=B_SPLINE_CURVE_WITH_KNOTS ( 'NONE', 3,
 ( #3464, #3362, #1956, #1257, #3733, #4093, #3413, #3785, #840, #2672, #513, #165, #1607, #1211, #3079, #2276, #3025, #231 ),
 .UNSPECIFIED., .F., .F.,
 ( 4, 2, 2, 2, 2, 2, 2, 2, 4 ),
 ( 0.005610345619348811042, 0.006311274135232913807, 0.007012202651117017439, 0.007713131167001120204, 0.008414059682885222102, 0.009114988198769324867, 0.009815916714653427633, 0.01051684523053753040, 0.01121777374642162275 ),
 .UNSPECIFIED. ) ;
#4446=VECTOR ( 'NONE', #4491, 1000.000000000000000 ) ;
#4447=CARTESIAN_POINT ( 'NONE',  ( 18.74250723456195189, 0.004097986548670510577, 31.86762445358909446 ) ) ;
#4448=ORIENTED_EDGE ( 'NONE', *, *, #1440, .F. ) ;
#4453=CARTESIAN_POINT ( 'NONE',  ( 14.09171737252990653, 2.367226359320930396, 34.55865096437416639 ) ) ;
#4454=VERTEX_POINT ( 'NONE', #981 ) ;
#4458=CARTESIAN_POINT ( 'NONE',  ( -7.619992765438045268, 0.004097986548673348585, 31.86762445358908735 ) ) ;
#4459=COLOUR_RGB ( '', 0.31764706, 0.68627451, 0.89019608) ;
#4461=CARTESIAN_POINT ( 'NONE',  ( 11.90639837545767321, 7.901597986548669184, 17.15262445358908039 ) ) ;
#4465=DIRECTION ( 'NONE',  ( -1.000000000000000000, 0.000000000000000000, 0.000000000000000000 ) ) ;
#4469=CARTESIAN_POINT ( 'NONE',  ( -12.37116490068861197, -7.143402013451321864, 17.90262445358908039 ) ) ;
#4470=DIRECTION ( 'NONE',  ( -0.000000000000000000, -0.000000000000000000, 1.000000000000000000 ) ) ;
#4471=EDGE_LOOP ( 'NONE', ( #2101, #908, #2004, #3702, #1432, #4570, #4194, #2383, #3302, #3975, #3781, #2748, #465, #350, #4076, #2339 ) ) ;
#4472=CARTESIAN_POINT ( 'NONE',  ( 13.83943491502687628, -3.546271172620213186, 31.39737200185970067 ) ) ;
#4482=VECTOR ( 'NONE', #2585, 1000.000000000000000 ) ;
#4483=AXIS2_PLACEMENT_3D ( 'NONE', #3752, #129, #3704 ) ;
#4484=CARTESIAN_POINT ( 'NONE',  ( 3.573757234561953045, 0.004097986548672966078, 17.15262445358908039 ) ) ;
#4491=DIRECTION ( 'NONE',  ( 1.000000000000000000, -1.076498916035107744E-16, -0.000000000000000000 ) ) ;
#4492=CARTESIAN_POINT ( 'NONE',  ( -8.369992765438043492, 6.401597986548673624, 17.90262445358908039 ) ) ;
#4494=VERTEX_POINT ( 'NONE', #4012 ) ;
#4495=CARTESIAN_POINT ( 'NONE',  ( 12.27095928922004653, -7.314612587678752220, 17.41568789468882983 ) ) ;
#4498=CYLINDRICAL_SURFACE ( 'NONE', #4072, 3.573749999999999538 ) ;
#4499=VERTEX_POINT ( 'NONE', #2521 ) ;
#4501=EDGE_CURVE ( 'NONE', #2026, #1657, #1559, .T. ) ;
#4505=VERTEX_POINT ( 'NONE', #4321 ) ;
#4507=DIRECTION ( 'NONE',  ( 0.000000000000000000, -1.000000000000000000, 0.000000000000000000 ) ) ;
#4511=DIRECTION ( 'NONE',  ( 0.000000000000000000, 0.000000000000000000, 1.000000000000000000 ) ) ;
#4515=CARTESIAN_POINT ( 'NONE',  ( -4.762492765438045339, 0.004097986548673111795, 3.292624453589077405 ) ) ;
#4516=CARTESIAN_POINT ( 'NONE',  ( -13.94784670859836595, -3.095491346532870836, 30.07369728485308258 ) ) ;
#4517=EDGE_LOOP ( 'NONE', ( #4122, #819, #2538, #2800 ) ) ;
#4518=CARTESIAN_POINT ( 'NONE',  ( 3.573757234561953045, 0.004097986548672966078, 17.16762445358907385 ) ) ;
#4524=AXIS2_PLACEMENT_3D ( 'NONE', #10, #4249, #1462 ) ;
#4531=FACE_OUTER_BOUND ( 'NONE', #334, .T. ) ;
#4532=B_SPLINE_CURVE_WITH_KNOTS ( 'NONE', 3,
 ( #2890, #1095, #2466, #2445, #3542, #1073, #3630, #4315, #316, #3230, #3187, #3281, #1848, #4338, #1124, #4623, #3909, #686 ),
 .UNSPECIFIED., .F., .F.,
 ( 4, 2, 2, 2, 2, 2, 2, 2, 4 ),
 ( 0.005610428130223219997, 0.006311357680970762496, 0.007012287231718304994, 0.007713216782465847493, 0.008414146333213389992, 0.009115075883960932490, 0.009816005434708474989, 0.01051693498545601749, 0.01121786453620356172 ),
 .UNSPECIFIED. ) ;
#4537=CARTESIAN_POINT ( 'NONE',  ( -8.369992765438045268, -6.393402013451325416, 31.86762445358908735 ) ) ;
#4542=ADVANCED_FACE ( 'NONE', ( #368, #737 ), #3216, .F. ) ;
#4543=VERTEX_POINT ( 'NONE', #782 ) ;
#4544=CARTESIAN_POINT ( 'NONE',  ( 14.17129034133389887, -1.872963726008691987, 38.78036386370911259 ) ) ;
#4545=CARTESIAN_POINT ( 'NONE',  ( 7.234561953626996335E-06, 0.004097986548672528061, -10.04237554641092345 ) ) ;
#4548=ORIENTED_EDGE ( 'NONE', *, *, #3112, .F. ) ;
#4550=EDGE_LOOP ( 'NONE', ( #3465, #772, #426, #454 ) ) ;
#4555=CARTESIAN_POINT ( 'NONE',  ( 7.234561953626996335E-06, 0.004097986548672528061, -10.04237554641092345 ) ) ;
#4558=CARTESIAN_POINT ( 'NONE',  ( -17.48249276543803532, -7.143402013451323640, 31.86762445358908735 ) ) ;
#4565=AXIS2_PLACEMENT_3D ( 'NONE', #1567, #1915, #4073 ) ;
#4566=CARTESIAN_POINT ( 'NONE',  ( 13.66253305200464929, -4.180199888423482335, 37.66696981337765493 ) ) ;
#4567=EDGE_CURVE ( 'NONE', #2227, #1498, #3657, .T. ) ;
#4570=ORIENTED_EDGE ( 'NONE', *, *, #159, .T. ) ;
#4571=TOROIDAL_SURFACE ( 'NONE', #967, 1.500000000000000000, 0.7500000000000000000 ) ;
#4575=VERTEX_POINT ( 'NONE', #61 ) ;
#4577=LINE ( 'NONE', #4172, #3143 ) ;
#4581=DIRECTION ( 'NONE',  ( 1.000000000000000000, 0.000000000000000000, 0.000000000000000000 ) ) ;
#4588=VECTOR ( 'NONE', #965, 1000.000000000000000 ) ;
#4589=ORIENTED_EDGE ( 'NONE', *, *, #159, .F. ) ;
#4591=TOROIDAL_SURFACE ( 'NONE', #2553, 6.397499999999999964, 0.7500000000000000000 ) ;
#4593=VERTEX_POINT ( 'NONE', #2833 ) ;
#4594=ORIENTED_EDGE ( 'NONE', *, *, #183, .F. ) ;
#4600=DIRECTION ( 'NONE',  ( 1.076498916035107621E-16, -1.000000000000000000, 0.000000000000000000 ) ) ;
#4604=CARTESIAN_POINT ( 'NONE',  ( -11.96599325036756589, 7.811730032674823576, 17.15262445358908039 ) ) ;
#4605=DIRECTION ( 'NONE',  ( 0.000000000000000000, 0.000000000000000000, 1.000000000000000000 ) ) ;
#4607=LINE ( 'NONE', #4558, #1377 ) ;
#4608=EDGE_CURVE ( 'NONE', #4593, #2966, #2007, .T. ) ;
#4614=CARTESIAN_POINT ( 'NONE',  ( 13.93190780555705999, -3.194059953323518108, 38.27679835742612369 ) ) ;
#4616=CARTESIAN_POINT ( 'NONE',  ( -3.573742765438046476, 0.004097986548672528061, 17.16762445358907385 ) ) ;
#4620=VERTEX_POINT ( 'NONE', #714 ) ;
#4622=ORIENTED_EDGE ( 'NONE', *, *, #2701, .F. ) ;
#4623=CARTESIAN_POINT ( 'NONE',  ( -14.28158774459093117, 0.4750311026362873390, 28.31727528644927006 ) ) ;
#4630=PLANE ( 'NONE',  #1307 ) ;
#4634=DIRECTION ( 'NONE',  ( 1.000000000000000000, -1.076498916035107621E-16, 0.000000000000000000 ) ) ;
#4636=VERTEX_POINT ( 'NONE', #2645 ) ;
#4637=CARTESIAN_POINT ( 'NONE',  ( 13.83079258162059588, -3.601903900406878911, 38.05628366828691611 ) ) ;
#4638=DIRECTION ( 'NONE',  ( -0.7071067811865449082, 8.659560562354902043E-17, 0.7071067811865501263 ) ) ;
#4639=CIRCLE ( 'NONE', #1910, 4.762499999999999289 ) ;
#4642=AXIS2_PLACEMENT_3D ( 'NONE', #175, #1620, #3037 ) ;
#4646=VECTOR ( 'NONE', #3686, 1000.000000000000000 ) ;
#4649=VERTEX_POINT ( 'NONE', #4393 ) ;
ENDSEC;
END-ISO-10303-21;
